ISO-10303-21;
HEADER;
FILE_DESCRIPTION (('STEP AP214'),
    '1' );
FILE_NAME ('Part 32,2_Varsayılan.step',
    '2026-10-10T17:45:43',
    ( '' ),
    ( '' ),
    'SwSTEP 2.0',
    'SolidWorks 2024',
    '' );
FILE_SCHEMA (( 'AUTOMOTIVE_DESIGN' ));
ENDSEC;

DATA;
#2=FACE_OUTER_BOUND ( 'NONE', #4262, .T. ) ;
#3=FACE_OUTER_BOUND ( 'NONE', #4088, .T. ) ;
#8=EDGE_CURVE ( 'NONE', #1209, #6017, #4433, .T. ) ;
#12=VERTEX_POINT ( 'NONE', #3966 ) ;
#26=CARTESIAN_POINT ( 'NONE',  ( 12.21008954351328413, -21.81796696573389127, 5.154724438801038922 ) ) ;
#31=CARTESIAN_POINT ( 'NONE',  ( -6.979603745006294879, -21.91560538710199779, 29.02082494059217765 ) ) ;
#33=CARTESIAN_POINT ( 'NONE',  ( 20.00000000000000000, 2.449293598294706513E-15, 39.00000000000001421 ) ) ;
#38=B_SPLINE_CURVE_WITH_KNOTS ( 'NONE', 3,
 ( #1697, #6029, #719, #3151, #3705, #4112 ),
 .UNSPECIFIED., .F., .F.,
 ( 4, 2, 4 ),
 ( 0.002032958594636734458, 0.003043324567219494060, 0.004053690539802253662 ),
 .UNSPECIFIED. ) ;
#39=B_SPLINE_CURVE_WITH_KNOTS ( 'NONE', 3,
 ( #3746, #4279, #1287, #1358, #4178, #783, #2350, #6257, #5782, #1842, #3804, #4739, #3314, #2826, #6155, #5224, #4801, #3253, #3221, #2727, #816, #3709, #5194, #4704, #300, #337, #4247, #6228, #4964, #531, #2445, #3864, #5907, #2482, #4446, #3838, #2858, #3480, #4377, #429, #1973, #1033 ),
 .UNSPECIFIED., .F., .F.,
 ( 4, 2, 2, 2, 2, 2, 2, 2, 2, 2, 2, 2, 2, 2, 2, 2, 2, 2, 2, 2, 4 ),
 ( 0.02358501416070326803, 0.02505868070871360154, 0.02653234725672393851, 0.02800601380473427202, 0.02947968035274460899, 0.03021651362674978442, 0.03095334690075495637, 0.03242701344876530722, 0.03390067999677565114, 0.03463751327078083003, 0.03537434654478600199, 0.03684801309279635284, 0.03758484636680152480, 0.03832167964080669675, 0.03979534618881705454, 0.04126901273682739846, 0.04200584601083257735, 0.04274267928483775625, 0.04421634583284810710, 0.04569001238085845795, 0.04716367892886881574 ),
 .UNSPECIFIED. ) ;
#44=CARTESIAN_POINT ( 'NONE',  ( 15.23842499831731523, 17.23716120365648052, 1.424676953056493112 ) ) ;
#53=VERTEX_POINT ( 'NONE', #142 ) ;
#54=CARTESIAN_POINT ( 'NONE',  ( 15.99408614349810698, 25.00000000000000000, 0.000000000000000000 ) ) ;
#56=CARTESIAN_POINT ( 'NONE',  ( -10.32035317195590984, -22.78260342671239869, 6.723738260341698414 ) ) ;
#59=CARTESIAN_POINT ( 'NONE',  ( -7.460990961498263019, -21.75625611239105694, 30.97809455494030928 ) ) ;
#64=B_SPLINE_CURVE_WITH_KNOTS ( 'NONE', 3,
 ( #996, #2949, #3883, #2468, #3228, #4436, #1895, #26, #1990, #4334, #964, #3954, #5828, #5441, #1405, #4365, #5381, #2913, #1023, #549, #5470, #2986, #4820, #446, #5345, #3979, #3401, #2885, #1536, #6336, #4954, #5863, #2503, #4462, #1441, #56, #4887, #4402, #1076, #3622, #4555, #3530, #1685, #4981, #1140, #4096 ),
 .UNSPECIFIED., .F., .F.,
 ( 4, 2, 2, 2, 2, 2, 2, 2, 2, 2, 2, 2, 2, 2, 2, 2, 2, 2, 2, 2, 2, 2, 4 ),
 ( 9.772241184477329324E-19, 0.002589099528182565047, 0.005178199056365129227, 0.006472748820456409799, 0.007767298584547690371, 0.01035639811273024805, 0.01294549764091280919, 0.01424004740500408803, 0.01553459716909536686, 0.01812369669727792107, 0.01941824646136919991, 0.02071279622546047527, 0.02330189575364303295, 0.02459644551773431179, 0.02589099528182559062, 0.02848009481000814483, 0.02977464457409942367, 0.03106919433819069556, 0.03365829386637325671, 0.03495284363046453902, 0.03624739339455581438, 0.03883649292273837206, 0.04142559245092092279 ),
 .UNSPECIFIED. ) ;
#75=CARTESIAN_POINT ( 'NONE',  ( -0.4497709217647500868, 23.00000000000000355, 24.27501000028010836 ) ) ;
#84=DIRECTION ( 'NONE',  ( 0.000000000000000000, -1.000000000000000000, 0.000000000000000000 ) ) ;
#92=CARTESIAN_POINT ( 'NONE',  ( -1.353316873173488588, -19.96515186930334096, 39.18355504947043499 ) ) ;
#93=AXIS2_PLACEMENT_3D ( 'NONE', #1355, #6255, #2382 ) ;
#110=CARTESIAN_POINT ( 'NONE',  ( 0.2247101425308446754, 23.00000000000000355, 24.27501000028010480 ) ) ;
#113=DIRECTION ( 'NONE',  ( 0.000000000000000000, 0.000000000000000000, -1.000000000000000000 ) ) ;
#116=VERTEX_POINT ( 'NONE', #626 ) ;
#123=CARTESIAN_POINT ( 'NONE',  ( 2.012341796004660122, 22.91179784512888773, 39.00000000000001421 ) ) ;
#136=UNCERTAINTY_MEASURE_WITH_UNIT (LENGTH_MEASURE( 1.000000000000000082E-05 ), #2437, 'distance_accuracy_value', 'NONE');
#138=CYLINDRICAL_SURFACE ( 'NONE', #419, 23.00000000000000000 ) ;
#141=CIRCLE ( 'NONE', #963, 25.00000000000000000 ) ;
#142=CARTESIAN_POINT ( 'NONE',  ( -25.00000000000000000, 0.000000000000000000, 0.000000000000000000 ) ) ;
#143=CARTESIAN_POINT ( 'NONE',  ( -7.491878387983184062, 21.74571065617575982, 31.20484628725278498 ) ) ;
#144=CARTESIAN_POINT ( 'NONE',  ( 1.698285149303728536, 24.95717370495093945, 9.939986931234113143 ) ) ;
#150=B_SPLINE_CURVE_WITH_KNOTS ( 'NONE', 3,
 ( #3485, #592, #44, #5457, #3004, #2543, #6001, #2576, #4969, #1575, #4536, #5913, #2094, #979, #2927, #4904, #500, #2450, #1978, #2215, #721, #6123, #4046, #6065, #6032, #5579, #1121, #5643, #2608, #6153, #5126, #1608, #754, #297, #3573, #3219, #1740, #5192, #1644, #234, #5544, #4175 ),
 .UNSPECIFIED., .F., .F.,
 ( 4, 2, 2, 2, 2, 2, 2, 2, 2, 2, 2, 2, 2, 2, 2, 2, 2, 2, 2, 2, 4 ),
 ( 0.000000000000000000, 0.002617858692138167777, 0.005235717384276335554, 0.006544646730345418141, 0.007853576076414500728, 0.01047143476855266243, 0.01308929346069082240, 0.01439822280675990239, 0.01570715215282898758, 0.01832501084496714408, 0.01963394019103622407, 0.02094286953710530058, 0.02356072822924346055, 0.02486965757531254054, 0.02617858692138162399, 0.02879644561351977702, 0.03141430430565794046, 0.03403216299779609350, 0.03665002168993425347, 0.03926788038207241344, 0.04188573907421057341 ),
 .UNSPECIFIED. ) ;
#160=LINE ( 'NONE', #6020, #2209 ) ;
#162=CARTESIAN_POINT ( 'NONE',  ( 0.000000000000000000, 0.000000000000000000, 51.00000000000002842 ) ) ;
#170=FACE_OUTER_BOUND ( 'NONE', #5424, .T. ) ;
#174=CARTESIAN_POINT ( 'NONE',  ( -7.269041597172756219, 21.82161019007790514, 29.87399971471650062 ) ) ;
#176=CARTESIAN_POINT ( 'NONE',  ( -5.944036167333009324, 24.28654258472968763, 8.982995935198127668 ) ) ;
#190=CARTESIAN_POINT ( 'NONE',  ( -2.450084894395748503, -22.87335089571185875, 38.87807751528530531 ) ) ;
#196=EDGE_CURVE ( 'NONE', #1460, #3708, #4019, .T. ) ;
#197=ADVANCED_FACE ( 'NONE', ( #3287 ), #5676, .F. ) ;
#200=AXIS2_PLACEMENT_3D ( 'NONE', #653, #2670, #3094 ) ;
#202=CARTESIAN_POINT ( 'NONE',  ( 0.000000000000000000, 0.000000000000000000, 0.000000000000000000 ) ) ;
#207=CARTESIAN_POINT ( 'NONE',  ( -3.466163672723409750, 22.74070890941651157, 25.10873389944362444 ) ) ;
#209=CIRCLE ( 'NONE', #6273, 23.00000000000000000 ) ;
#210=CARTESIAN_POINT ( 'NONE',  ( -13.06023069425439509, 21.31967003585100784, 4.296371343529790110 ) ) ;
#211=CARTESIAN_POINT ( 'NONE',  ( 3.471216600621237713, -22.73745234227088829, 38.42710443719838054 ) ) ;
#219=CYLINDRICAL_SURFACE ( 'NONE', #1741, 17.79053956122086078 ) ;
#222=EDGE_CURVE ( 'NONE', #2940, #959, #39, .T. ) ;
#223=CARTESIAN_POINT ( 'NONE',  ( -15.63711455316257215, -16.87386736187478675, 0.7328676451471519693 ) ) ;
#234=CARTESIAN_POINT ( 'NONE',  ( -15.23263781889692048, 17.24245498722747527, 1.434805278142651463 ) ) ;
#237=DIRECTION ( 'NONE',  ( -1.000000000000000000, 0.000000000000000000, 0.000000000000000000 ) ) ;
#243=CARTESIAN_POINT ( 'NONE',  ( 0.000000000000000000, 0.000000000000000000, 55.00000000000000711 ) ) ;
#246=EDGE_LOOP ( 'NONE', ( #2762, #958, #1397, #4692, #5981, #2970 ) ) ;
#252=DIRECTION ( 'NONE',  ( 1.000000000000000000, 0.000000000000000000, 0.000000000000000000 ) ) ;
#255=ADVANCED_FACE ( 'NONE', ( #6347, #3897 ), #5362, .T. ) ;
#259=DIRECTION ( 'NONE',  ( 0.000000000000000000, 0.000000000000000000, 1.000000000000000000 ) ) ;
#264=EDGE_CURVE ( 'NONE', #775, #6000, #3921, .T. ) ;
#265=CARTESIAN_POINT ( 'NONE',  ( 10.97130857767020551, 22.47473234318869828, 6.237739505811246588 ) ) ;
#266=CARTESIAN_POINT ( 'NONE',  ( 5.116921499885075164, -22.42580359959007552, 37.27629952662707069 ) ) ;
#270=CARTESIAN_POINT ( 'NONE',  ( -0.4986381067920973575, 25.00000000000001066, 24.27501000028010836 ) ) ;
#274=CARTESIAN_POINT ( 'NONE',  ( 0.000000000000000000, 0.000000000000000000, 44.00000000000000711 ) ) ;
#279=ORIENTED_EDGE ( 'NONE', *, *, #1801, .T. ) ;
#283=CARTESIAN_POINT ( 'NONE',  ( 10.37037532854004418, -20.54332595864094202, 6.688011403969689184 ) ) ;
#284=CIRCLE ( 'NONE', #4395, 22.00000000000000000 ) ;
#288=VECTOR ( 'NONE', #565, 1000.000000000000000 ) ;
#290=CARTESIAN_POINT ( 'NONE',  ( 0.000000000000000000, 0.000000000000000000, 0.000000000000000000 ) ) ;
#294=AXIS2_PLACEMENT_3D ( 'NONE', #2245, #5189, #5257 ) ;
#295=CARTESIAN_POINT ( 'NONE',  ( -2.426466830553623222, -24.88612820222272148, 38.88851386838337731 ) ) ;
#297=CARTESIAN_POINT ( 'NONE',  ( -10.37037532854004418, 20.54332595864094202, 6.688011403969689184 ) ) ;
#300=CARTESIAN_POINT ( 'NONE',  ( 7.246617758453442804, 23.92680898849839721, 29.82624669321133126 ) ) ;
#304=CARTESIAN_POINT ( 'NONE',  ( 7.306265819825862096, -23.90859775135293219, 30.06340984243352921 ) ) ;
#307=CARTESIAN_POINT ( 'NONE',  ( -3.336113272159680676, 24.78061407909199687, 25.03989924742864304 ) ) ;
#308=VECTOR ( 'NONE', #2366, 1000.000000000000000 ) ;
#309=VECTOR ( 'NONE', #6106, 1000.000000000000000 ) ;
#310=DIRECTION ( 'NONE',  ( 1.000000000000000000, 0.000000000000000000, 0.000000000000000000 ) ) ;
#311=CIRCLE ( 'NONE', #916, 25.00000000000000000 ) ;
#323=CARTESIAN_POINT ( 'NONE',  ( -4.378668635177231927, -22.59503479412315485, 9.474032806803469597 ) ) ;
#324=ORIENTED_EDGE ( 'NONE', *, *, #5982, .T. ) ;
#337=CARTESIAN_POINT ( 'NONE',  ( 7.102515314070983798, 23.96997983984566361, 29.35314634237167297 ) ) ;
#340=CARTESIAN_POINT ( 'NONE',  ( 7.059265739357024394, -21.89000174688035827, 29.23188816227238362 ) ) ;
#343=CARTESIAN_POINT ( 'NONE',  ( -0.4915545007834206670, 24.99637963107063499, 39.26296923598712851 ) ) ;
#348=ORIENTED_EDGE ( 'NONE', *, *, #5467, .F. ) ;
#351=CARTESIAN_POINT ( 'NONE',  ( 0.000000000000000000, 0.000000000000000000, 0.000000000000000000 ) ) ;
#352=CARTESIAN_POINT ( 'NONE',  ( 3.009099790203600300, -22.80648947684007410, 9.749155414846011780 ) ) ;
#354=EDGE_LOOP ( 'NONE', ( #837, #2657 ) ) ;
#355=DIRECTION ( 'NONE',  ( -1.000000000000000000, 0.000000000000000000, 0.000000000000000000 ) ) ;
#356=ORIENTED_EDGE ( 'NONE', *, *, #2582, .T. ) ;
#358=EDGE_CURVE ( 'NONE', #4881, #53, #311, .T. ) ;
#359=DIRECTION ( 'NONE',  ( 0.000000000000000000, 0.000000000000000000, 1.000000000000000000 ) ) ;
#361=CARTESIAN_POINT ( 'NONE',  ( -4.953190041214019068, -24.50516424074860922, 26.13799397941500757 ) ) ;
#365=MANIFOLD_SOLID_BREP ( 'Cut-Extrude4', #5984 ) ;
#369=CARTESIAN_POINT ( 'NONE',  ( 7.450717329638294473, -23.86413627455948117, 32.76425935539838008 ) ) ;
#372=CARTESIAN_POINT ( 'NONE',  ( -7.499773188859400364, 23.84855136421925437, 31.27916535100971274 ) ) ;
#373=DIRECTION ( 'NONE',  ( 0.000000000000000000, 0.000000000000000000, 1.000000000000000000 ) ) ;
#374=DIRECTION ( 'NONE',  ( 1.000000000000000000, 0.000000000000000000, 0.000000000000000000 ) ) ;
#377=AXIS2_PLACEMENT_3D ( 'NONE', #2646, #5558, #3130 ) ;
#379=ORIENTED_EDGE ( 'NONE', *, *, #464, .T. ) ;
#392=DIRECTION ( 'NONE',  ( -0.000000000000000000, -0.000000000000000000, -1.000000000000000000 ) ) ;
#393=CARTESIAN_POINT ( 'NONE',  ( 9.184177739184520255E-16, -25.00000000000000000, 39.27501000028010480 ) ) ;
#394=VERTEX_POINT ( 'NONE', #2235 ) ;
#397=AXIS2_PLACEMENT_3D ( 'NONE', #5759, #4256, #374 ) ;
#403=CARTESIAN_POINT ( 'NONE',  ( 6.830924868230229485, -24.04887075291642873, 34.88135594814354334 ) ) ;
#404=ORIENTED_EDGE ( 'NONE', *, *, #2795, .F. ) ;
#408=CARTESIAN_POINT ( 'NONE',  ( -6.096488593930904365, 24.24566755320543976, 36.15017996222949392 ) ) ;
#413=EDGE_LOOP ( 'NONE', ( #6163, #678, #2072, #1728, #5455, #5735 ) ) ;
#414=VERTEX_POINT ( 'NONE', #4884 ) ;
#419=AXIS2_PLACEMENT_3D ( 'NONE', #4172, #1605, #6062 ) ;
#420=DIRECTION ( 'NONE',  ( 0.000000000000000000, 0.000000000000000000, 1.000000000000000000 ) ) ;
#424=CARTESIAN_POINT ( 'NONE',  ( -5.575863217335945698, -22.31445838370337853, 26.75407420319146823 ) ) ;
#429=CARTESIAN_POINT ( 'NONE',  ( 0.9889208576060609657, 24.98510605705583743, 24.32423630022272576 ) ) ;
#430=CARTESIAN_POINT ( 'NONE',  ( 0.000000000000000000, 0.000000000000000000, 50.00000000000000711 ) ) ;
#431=CARTESIAN_POINT ( 'NONE',  ( 7.443729366988918004E-21, -23.00000000000000000, 24.27501000028010125 ) ) ;
#433=FACE_OUTER_BOUND ( 'NONE', #246, .T. ) ;
#435=CARTESIAN_POINT ( 'NONE',  ( -5.723282545231354490, 22.27700230555918992, 36.62722877095559681 ) ) ;
#437=CARTESIAN_POINT ( 'NONE',  ( 0.000000000000000000, 0.000000000000000000, 39.00000000000001421 ) ) ;
#438=DIRECTION ( 'NONE',  ( -0.000000000000000000, -0.000000000000000000, -1.000000000000000000 ) ) ;
#440=ORIENTED_EDGE ( 'NONE', *, *, #1522, .T. ) ;
#442=LINE ( 'NONE', #6275, #1455 ) ;
#444=DIRECTION ( 'NONE',  ( -0.000000000000000000, -0.000000000000000000, -1.000000000000000000 ) ) ;
#445=AXIS2_PLACEMENT_3D ( 'NONE', #503, #6298, #3844 ) ;
#446=CARTESIAN_POINT ( 'NONE',  ( -0.8363506376998798286, -25.00098981342394922, 10.00139094947510721 ) ) ;
#448=DIRECTION ( 'NONE',  ( 0.000000000000000000, 0.000000000000000000, -1.000000000000000000 ) ) ;
#449=( NAMED_UNIT ( * ) PLANE_ANGLE_UNIT ( ) SI_UNIT ( $, .RADIAN. ) );
#450=CARTESIAN_POINT ( 'NONE',  ( 7.443729366988918004E-21, -23.00000000000000000, 24.27501000028010125 ) ) ;
#451=DIRECTION ( 'NONE',  ( 0.000000000000000000, 0.000000000000000000, 1.000000000000000000 ) ) ;
#459=EDGE_LOOP ( 'NONE', ( #5395, #324, #5477, #2014 ) ) ;
#462=CARTESIAN_POINT ( 'NONE',  ( -2.869322346082823660, 22.82391999846087316, 38.71877048136666843 ) ) ;
#464=EDGE_CURVE ( 'NONE', #6000, #1209, #1438, .T. ) ;
#466=ADVANCED_FACE ( 'NONE', ( #4852 ), #5892, .T. ) ;
#470=ORIENTED_EDGE ( 'NONE', *, *, #1913, .T. ) ;
#478=CARTESIAN_POINT ( 'NONE',  ( 25.00000000000000000, 3.061616997868383043E-15, 41.00000000000000000 ) ) ;
#481=ORIENTED_EDGE ( 'NONE', *, *, #1052, .T. ) ;
#482=EDGE_CURVE ( 'NONE', #1816, #1146, #442, .T. ) ;
#491=CARTESIAN_POINT ( 'NONE',  ( 2.012341796004660122, 19.89850447888114005, 39.00000000000001421 ) ) ;
#498=EDGE_LOOP ( 'NONE', ( #6199, #5221 ) ) ;
#500=CARTESIAN_POINT ( 'NONE',  ( 5.608440128082920140, 22.30969483029271672, 9.098285821462422263 ) ) ;
#503=CARTESIAN_POINT ( 'NONE',  ( 0.000000000000000000, 0.000000000000000000, 47.00000000000000711 ) ) ;
#504=CIRCLE ( 'NONE', #397, 22.00000000000000000 ) ;
#511=ORIENTED_EDGE ( 'NONE', *, *, #8, .F. ) ;
#514=ADVANCED_FACE ( 'NONE', ( #1956 ), #5797, .T. ) ;
#519=ORIENTED_EDGE ( 'NONE', *, *, #1522, .F. ) ;
#524=CARTESIAN_POINT ( 'NONE',  ( 15.99408614349810698, -19.21429697996681440, 0.000000000000000000 ) ) ;
#531=CARTESIAN_POINT ( 'NONE',  ( 5.958576596270775738, 24.28117850353844531, 27.19366677815228783 ) ) ;
#532=CIRCLE ( 'NONE', #4010, 22.00000000000000000 ) ;
#538=AXIS2_PLACEMENT_3D ( 'NONE', #4344, #1903, #5392 ) ;
#544=ORIENTED_EDGE ( 'NONE', *, *, #222, .T. ) ;
#545=CIRCLE ( 'NONE', #4854, 23.00000000000000000 ) ;
#549=CARTESIAN_POINT ( 'NONE',  ( 2.201053925086813301, -24.90665284231784327, 9.868642342566223746 ) ) ;
#554=VERTEX_POINT ( 'NONE', #4298 ) ;
#559=DIRECTION ( 'NONE',  ( 1.000000000000000000, 0.000000000000000000, 0.000000000000000000 ) ) ;
#562=CARTESIAN_POINT ( 'NONE',  ( 0.000000000000000000, 0.000000000000000000, 41.00000000000000000 ) ) ;
#563=CARTESIAN_POINT ( 'NONE',  ( -6.385057176062306716, 22.09706105569707191, 27.81520467947423114 ) ) ;
#565=DIRECTION ( 'NONE',  ( -0.000000000000000000, -0.000000000000000000, -1.000000000000000000 ) ) ;
#575=B_SPLINE_CURVE_WITH_KNOTS ( 'NONE', 3,
 ( #393, #6286, #1900, #2347, #295, #3772, #5741, #3216, #2380, #3743, #1839, #2282, #1873, #4243, #1314, #2246, #812, #4735, #5805, #6224, #877, #5703, #1772, #2316, #3311, #2823, #903, #6190, #5778, #5259, #845, #4308, #361, #2798, #3800, #4273, #1283, #5672, #3248, #5220, #5292, #3834 ),
 .UNSPECIFIED., .F., .F.,
 ( 4, 2, 2, 2, 2, 2, 2, 2, 2, 2, 2, 2, 2, 2, 2, 2, 2, 2, 2, 2, 4 ),
 ( 0.02358501416070326456, 0.02505868070871361541, 0.02653234725672396974, 0.02800601380473432406, 0.02947968035274467491, 0.03021651362674985727, 0.03095334690075503964, 0.03242701344876540437, 0.03390067999677577604, 0.03463751327078095493, 0.03537434654478614077, 0.03684801309279646386, 0.03758484636680162194, 0.03832167964080678696, 0.03979534618881712393, 0.04126901273682745397, 0.04200584601083262593, 0.04274267928483779788, 0.04421634583284814179, 0.04569001238085847877, 0.04716367892886881574 ),
 .UNSPECIFIED. ) ;
#578=CARTESIAN_POINT ( 'NONE',  ( -6.497654244294650105, -22.06338186837085402, 35.52745571863555085 ) ) ;
#581=ORIENTED_EDGE ( 'NONE', *, *, #6309, .F. ) ;
#583=FACE_BOUND ( 'NONE', #2042, .T. ) ;
#586=DIRECTION ( 'NONE',  ( 1.000000000000000000, 0.000000000000000000, -0.000000000000000000 ) ) ;
#592=CARTESIAN_POINT ( 'NONE',  ( 15.63711455316257215, 16.87386736187478675, 0.7328676451471519693 ) ) ;
#593=ORIENTED_EDGE ( 'NONE', *, *, #669, .F. ) ;
#594=CARTESIAN_POINT ( 'NONE',  ( 3.065100562737908430, 22.79875969907089228, 24.91526600425119042 ) ) ;
#599=DIRECTION ( 'NONE',  ( 1.000000000000000000, 0.000000000000000000, 0.000000000000000000 ) ) ;
#609=CARTESIAN_POINT ( 'NONE',  ( 0.000000000000000000, 0.000000000000000000, 39.00000000000001421 ) ) ;
#610=CIRCLE ( 'NONE', #2025, 25.00000000000000000 ) ;
#626=CARTESIAN_POINT ( 'NONE',  ( 1.908796811648538206E-15, -20.00000000000000711, 39.27501000028011902 ) ) ;
#627=CARTESIAN_POINT ( 'NONE',  ( -7.471932569767337995, 21.75248695045747382, 32.56440574765390039 ) ) ;
#629=CARTESIAN_POINT ( 'NONE',  ( -14.34088693563092320, 20.48519421429849174, 2.767956487184815462 ) ) ;
#635=VERTEX_POINT ( 'NONE', #123 ) ;
#638=AXIS2_PLACEMENT_3D ( 'NONE', #1399, #3918, #2463 ) ;
#641=CARTESIAN_POINT ( 'NONE',  ( 0.000000000000000000, 0.000000000000000000, 50.00000000000000711 ) ) ;
#653=CARTESIAN_POINT ( 'NONE',  ( 0.000000000000000000, 0.000000000000000000, 23.77500997278103512 ) ) ;
#656=CARTESIAN_POINT ( 'NONE',  ( 6.381573266039188397, 22.09732860014628031, 35.72159715675526570 ) ) ;
#669=EDGE_CURVE ( 'NONE', #394, #1346, #2015, .T. ) ;
#678=ORIENTED_EDGE ( 'NONE', *, *, #2302, .T. ) ;
#689=CARTESIAN_POINT ( 'NONE',  ( 7.368286983821151992, 21.78790057683621129, 30.30389194166913569 ) ) ;
#690=VECTOR ( 'NONE', #2330, 1000.000000000000000 ) ;
#692=CARTESIAN_POINT ( 'NONE',  ( 9.287558414957929998, 23.21379839259252620, 7.388795739543629004 ) ) ;
#703=CARTESIAN_POINT ( 'NONE',  ( 20.00000000000000000, 2.449293598294706513E-15, 51.00000000000002842 ) ) ;
#706=ORIENTED_EDGE ( 'NONE', *, *, #4636, .T. ) ;
#712=DIRECTION ( 'NONE',  ( 0.000000000000000000, 0.000000000000000000, -1.000000000000000000 ) ) ;
#717=CIRCLE ( 'NONE', #200, 40.00000002749906258 ) ;
#719=CARTESIAN_POINT ( 'NONE',  ( 0.6815295361380621086, -19.99121204295638776, 39.25166565497248428 ) ) ;
#720=ORIENTED_EDGE ( 'NONE', *, *, #5167, .T. ) ;
#721=CARTESIAN_POINT ( 'NONE',  ( 1.798140372219934502, 22.93384243835984648, 9.914400014297026331 ) ) ;
#728=CARTESIAN_POINT ( 'NONE',  ( 2.450350183182338881, -22.87332759541404670, 38.87800362567253387 ) ) ;
#732=CARTESIAN_POINT ( 'NONE',  ( -2.012341796004660122, -19.89850447888114005, 39.00000000000001421 ) ) ;
#733=CARTESIAN_POINT ( 'NONE',  ( -22.00000000000000000, 0.000000000000000000, 44.00000000000000711 ) ) ;
#736=FACE_OUTER_BOUND ( 'NONE', #1045, .T. ) ;
#739=( GEOMETRIC_REPRESENTATION_CONTEXT ( 3 ) GLOBAL_UNCERTAINTY_ASSIGNED_CONTEXT ( ( #3662 ) ) GLOBAL_UNIT_ASSIGNED_CONTEXT ( ( #2204, #1242, #2172 ) ) REPRESENTATION_CONTEXT ( 'NONE', 'WORKASPACE' ) );
#741=CARTESIAN_POINT ( 'NONE',  ( 11.01859089670589675, -20.20136408472527023, 6.200517937480644726 ) ) ;
#751=ORIENTED_EDGE ( 'NONE', *, *, #944, .F. ) ;
#753=EDGE_CURVE ( 'NONE', #861, #3440, #3680, .T. ) ;
#754=CARTESIAN_POINT ( 'NONE',  ( -8.997257985596670338, 21.18070524412206623, 7.578991052498396996 ) ) ;
#758=CARTESIAN_POINT ( 'NONE',  ( 0.8363506376998767200, 25.00098981342395277, 10.00139094947511076 ) ) ;
#759=CARTESIAN_POINT ( 'NONE',  ( 7.411490251847205002, -21.77340291014862217, 33.00915547857365340 ) ) ;
#761=ORIENTED_EDGE ( 'NONE', *, *, #2998, .F. ) ;
#762=CARTESIAN_POINT ( 'NONE',  ( -7.450717329638298914, 23.86413627455948472, 32.76425935539839429 ) ) ;
#763=DIRECTION ( 'NONE',  ( -1.000000000000000000, 0.000000000000000000, 0.000000000000000000 ) ) ;
#765=DIRECTION ( 'NONE',  ( -1.000000000000000000, 0.000000000000000000, 0.000000000000000000 ) ) ;
#766=ORIENTED_EDGE ( 'NONE', *, *, #3453, .F. ) ;
#770=DIRECTION ( 'NONE',  ( -0.000000000000000000, -0.000000000000000000, -1.000000000000000000 ) ) ;
#775=VERTEX_POINT ( 'NONE', #733 ) ;
#781=DIRECTION ( 'NONE',  ( 1.000000000000000000, 0.000000000000000000, 0.000000000000000000 ) ) ;
#783=CARTESIAN_POINT ( 'NONE',  ( 3.330617891528926844, 24.78132568362453370, 38.51271458136145753 ) ) ;
#791=EDGE_CURVE ( 'NONE', #6038, #1386, #6343, .T. ) ;
#792=CARTESIAN_POINT ( 'NONE',  ( -4.375754180095210444, 24.61494036324240398, 25.67889403490023881 ) ) ;
#794=CARTESIAN_POINT ( 'NONE',  ( -15.99408614349810698, -19.21429697996681440, -4.336808689942017736E-15 ) ) ;
#796=ADVANCED_FACE ( 'NONE', ( #4678 ), #5202, .T. ) ;
#797=AXIS2_PLACEMENT_3D ( 'NONE', #2741, #3618, #310 ) ;
#804=CARTESIAN_POINT ( 'NONE',  ( -8.336125322366124024, -21.45114114349586387, 7.948328953041721157 ) ) ;
#807=ORIENTED_EDGE ( 'NONE', *, *, #3257, .T. ) ;
#812=CARTESIAN_POINT ( 'NONE',  ( -7.257437786822881876, -23.92362332953076276, 33.72945147699582691 ) ) ;
#816=CARTESIAN_POINT ( 'NONE',  ( 7.499981071996971949, 23.84848598800518715, 32.02274772221157662 ) ) ;
#817=CARTESIAN_POINT ( 'NONE',  ( 4.061217559732478222, 22.64157742495655512, 38.09601054039983836 ) ) ;
#818=CIRCLE ( 'NONE', #93, 23.00000000000000000 ) ;
#820=CARTESIAN_POINT ( 'NONE',  ( 3.336113272159680232, -24.78061407909199332, 25.03989924742863948 ) ) ;
#824=CARTESIAN_POINT ( 'NONE',  ( -0.9883880857196325476, 24.98510658176930832, 24.32423833034778937 ) ) ;
#829=VECTOR ( 'NONE', #2966, 1000.000000000000000 ) ;
#832=ORIENTED_EDGE ( 'NONE', *, *, #6189, .T. ) ;
#834=AXIS2_PLACEMENT_3D ( 'NONE', #162, #1208, #5153 ) ;
#835=CARTESIAN_POINT ( 'NONE',  ( 5.943311860187945328, -22.23481035324009270, 8.999810584836245297 ) ) ;
#836=CARTESIAN_POINT ( 'NONE',  ( -15.99408614349810698, 19.21429697996681796, -4.336808689942017736E-15 ) ) ;
#837=ORIENTED_EDGE ( 'NONE', *, *, #4553, .F. ) ;
#845=CARTESIAN_POINT ( 'NONE',  ( -5.649026277996909151, -24.35594688685564790, 26.81770774654597744 ) ) ;
#850=CARTESIAN_POINT ( 'NONE',  ( -7.182657412981705209E-17, 20.00000000000000711, 39.27501000028011902 ) ) ;
#852=DIRECTION ( 'NONE',  ( 0.000000000000000000, 0.000000000000000000, -1.000000000000000000 ) ) ;
#853=CARTESIAN_POINT ( 'NONE',  ( 2.223777455422794702, -22.89327810718596368, 24.60873847605252251 ) ) ;
#857=DIRECTION ( 'NONE',  ( 0.000000000000000000, 0.000000000000000000, -1.000000000000000000 ) ) ;
#859=CARTESIAN_POINT ( 'NONE',  ( 0.000000000000000000, 0.000000000000000000, 51.00000000000002842 ) ) ;
#861=VERTEX_POINT ( 'NONE', #1656 ) ;
#865=EDGE_CURVE ( 'NONE', #1470, #4878, #3658, .T. ) ;
#867=APPLICATION_CONTEXT ( 'automotive_design' ) ;
#869=DIRECTION ( 'NONE',  ( 0.000000000000000000, -1.000000000000000000, 0.000000000000000000 ) ) ;
#872=EDGE_LOOP ( 'NONE', ( #950, #2470, #2429, #6101 ) ) ;
#877=CARTESIAN_POINT ( 'NONE',  ( -7.499981071996971949, -23.84848598800519426, 32.02274772221159083 ) ) ;
#878=ORIENTED_EDGE ( 'NONE', *, *, #5629, .F. ) ;
#883=CARTESIAN_POINT ( 'NONE',  ( 0.4986381067920973575, -25.00000000000001421, 24.27501000028011191 ) ) ;
#884=ORIENTED_EDGE ( 'NONE', *, *, #4544, .F. ) ;
#886=CARTESIAN_POINT ( 'NONE',  ( -1.957817464472356495, 24.92794428843967580, 39.03180047523679974 ) ) ;
#897=CYLINDRICAL_SURFACE ( 'NONE', #2061, 22.00000000000000000 ) ;
#900=AXIS2_PLACEMENT_3D ( 'NONE', #3588, #2957, #4370 ) ;
#901=CARTESIAN_POINT ( 'NONE',  ( -5.103812965180195782, -22.42723062334006556, 26.27493091522155666 ) ) ;
#903=CARTESIAN_POINT ( 'NONE',  ( -7.019376005445151279, -23.99453911528665984, 29.12205218481383540 ) ) ;
#910=CARTESIAN_POINT ( 'NONE',  ( 6.801000575755121069, -21.97168837322005075, 28.60528907419297084 ) ) ;
#915=CARTESIAN_POINT ( 'NONE',  ( -3.471216600621237713, 22.73745234227088829, 38.42710443719838054 ) ) ;
#916=AXIS2_PLACEMENT_3D ( 'NONE', #351, #3139, #6242 ) ;
#943=DIRECTION ( 'NONE',  ( -0.000000000000000000, -0.000000000000000000, -1.000000000000000000 ) ) ;
#944=EDGE_CURVE ( 'NONE', #2247, #635, #2364, .T. ) ;
#949=CARTESIAN_POINT ( 'NONE',  ( 4.240260142090316542, -22.60916465144881826, 25.57229111368760854 ) ) ;
#950=ORIENTED_EDGE ( 'NONE', *, *, #464, .F. ) ;
#953=CARTESIAN_POINT ( 'NONE',  ( -6.980300741495532257, 21.91538084489497962, 34.52732716285097325 ) ) ;
#958=ORIENTED_EDGE ( 'NONE', *, *, #1201, .F. ) ;
#959=VERTEX_POINT ( 'NONE', #5334 ) ;
#963=AXIS2_PLACEMENT_3D ( 'NONE', #3288, #3710, #5266 ) ;
#964=CARTESIAN_POINT ( 'NONE',  ( 10.34785354329971341, -22.76990768458740533, 6.703770685560596299 ) ) ;
#967=CARTESIAN_POINT ( 'NONE',  ( -7.210417624014669791, -21.84081640740546248, 33.88833234030835229 ) ) ;
#979=CARTESIAN_POINT ( 'NONE',  ( 7.200995294576264527, 21.84734027758491237, 8.482870732638906119 ) ) ;
#980=EDGE_CURVE ( 'NONE', #1773, #3440, #1187, .T. ) ;
#984=PLANE ( 'NONE',  #1975 ) ;
#989=EDGE_LOOP ( 'NONE', ( #5388, #3169 ) ) ;
#996=CARTESIAN_POINT ( 'NONE',  ( 15.99408614349810698, -19.21429697996681440, 0.000000000000000000 ) ) ;
#999=CARTESIAN_POINT ( 'NONE',  ( -0.2247101425308446754, -23.00000000000000355, 24.27501000028010480 ) ) ;
#1005=CARTESIAN_POINT ( 'NONE',  ( 0.000000000000000000, 0.000000000000000000, 47.00000000000000711 ) ) ;
#1007=CARTESIAN_POINT ( 'NONE',  ( 9.184177739184520255E-16, -25.00000000000000000, 39.27501000028010480 ) ) ;
#1020=VERTEX_POINT ( 'NONE', #4387 ) ;
#1023=CARTESIAN_POINT ( 'NONE',  ( 3.487686359055458762, -24.77054744280749432, 9.676329747922178370 ) ) ;
#1033=CARTESIAN_POINT ( 'NONE',  ( 2.546401178541497462E-16, 25.00000000000000000, 24.27501000028010125 ) ) ;
#1040=CARTESIAN_POINT ( 'NONE',  ( -5.576854706809766249, 22.31420130230918986, 36.79476692679597249 ) ) ;
#1045=EDGE_LOOP ( 'NONE', ( #2012, #5927, #2089, #1195 ) ) ;
#1050=PLANE ( 'NONE',  #1622 ) ;
#1052=EDGE_CURVE ( 'NONE', #635, #5193, #6086, .T. ) ;
#1063=EDGE_LOOP ( 'NONE', ( #4947, #720 ) ) ;
#1067=CARTESIAN_POINT ( 'NONE',  ( 6.383431969492757929, 22.09754339782970334, 27.81230622618427617 ) ) ;
#1072=ORIENTED_EDGE ( 'NONE', *, *, #980, .T. ) ;
#1076=CARTESIAN_POINT ( 'NONE',  ( -12.19460461707455678, -21.82662405552711959, 5.169298567843259917 ) ) ;
#1079=SHAPE_DEFINITION_REPRESENTATION ( #3636, #1490 ) ;
#1080=CARTESIAN_POINT ( 'NONE',  ( -4.061217559732478222, -22.64157742495655512, 38.09601054039983836 ) ) ;
#1081=DIRECTION ( 'NONE',  ( 0.000000000000000000, -1.000000000000000000, 0.000000000000000000 ) ) ;
#1091=CARTESIAN_POINT ( 'NONE',  ( 5.722301980643075048, 22.27724803853372393, 26.92170784547232998 ) ) ;
#1092=CARTESIAN_POINT ( 'NONE',  ( -12.21008954351328057, 21.81796696573388772, 5.154724438801039810 ) ) ;
#1094=ORIENTED_EDGE ( 'NONE', *, *, #2856, .F. ) ;
#1098=DIRECTION ( 'NONE',  ( -1.000000000000000000, 0.000000000000000000, 0.000000000000000000 ) ) ;
#1105=AXIS2_PLACEMENT_3D ( 'NONE', #1219, #259, #781 ) ;
#1109=CARTESIAN_POINT ( 'NONE',  ( 2.012341796004660122, -22.91179784512888773, 39.00000000000001421 ) ) ;
#1111=B_SPLINE_CURVE_WITH_KNOTS ( 'NONE', 3,
 ( #3716, #728, #6127, #211, #6071, #3674, #5583, #5680, #266, #5101, #6098, #2162, #4119, #2222, #3641, #5648, #1227, #3192, #5171, #759, #4183, #6159, #1815, #5845, #5328, #340, #5752, #910, #6232, #5785, #1361, #1779, #3840, #2862, #949, #5810, #5713, #2806, #853, #2255, #1423, #4840, #5231, #431 ),
 .UNSPECIFIED., .F., .F.,
 ( 4, 2, 2, 2, 2, 2, 2, 2, 2, 2, 2, 2, 2, 2, 2, 2, 2, 2, 2, 2, 2, 4 ),
 ( 0.000000000000000000, 0.001348713335717714561, 0.002023070003576572708, 0.002697426671435430422, 0.004046140007153132406, 0.004720496675011990988, 0.005394853342870850436, 0.006743566678588568467, 0.007417923346447437456, 0.008092280014306306446, 0.009440993350024065242, 0.01078970668574182230, 0.01213842002145957069, 0.01281277668931844402, 0.01348713335717731908, 0.01483584669289507441, 0.01618456002861283147, 0.01753327336433058506, 0.01888198670004834212, 0.01955634336790721892, 0.02023070003576609918, 0.02157941337148385624 ),
 .UNSPECIFIED. ) ;
#1116=ADVANCED_FACE ( 'NONE', ( #1181 ), #984, .T. ) ;
#1120=ORIENTED_EDGE ( 'NONE', *, *, #4636, .F. ) ;
#1121=CARTESIAN_POINT ( 'NONE',  ( -3.443445423526525051, 22.74486015987870147, 9.669004251864722121 ) ) ;
#1124=CARTESIAN_POINT ( 'NONE',  ( 7.210417624014669791, 21.84081640740546248, 33.88833234030835229 ) ) ;
#1132=ORIENTED_EDGE ( 'NONE', *, *, #4544, .T. ) ;
#1135=AXIS2_PLACEMENT_3D ( 'NONE', #3429, #5308, #2337 ) ;
#1139=CARTESIAN_POINT ( 'NONE',  ( 0.000000000000000000, 0.000000000000000000, 0.000000000000000000 ) ) ;
#1140=CARTESIAN_POINT ( 'NONE',  ( -15.63352991451900564, -19.51442596162454990, 0.7402269581920462027 ) ) ;
#1146=VERTEX_POINT ( 'NONE', #2632 ) ;
#1158=CARTESIAN_POINT ( 'NONE',  ( -7.260561981364187290, 21.82400181508864634, 33.66843689838669462 ) ) ;
#1164=CYLINDRICAL_SURFACE ( 'NONE', #5723, 20.00000000000000000 ) ;
#1177=ORIENTED_EDGE ( 'NONE', *, *, #1707, .T. ) ;
#1181=FACE_OUTER_BOUND ( 'NONE', #4413, .T. ) ;
#1186=CARTESIAN_POINT ( 'NONE',  ( -1.790150932673403750, 22.93126094008908566, 24.48831024192238814 ) ) ;
#1187=CIRCLE ( 'NONE', #2629, 20.00000000000000000 ) ;
#1189=CARTESIAN_POINT ( 'NONE',  ( 10.32035317195591517, 22.78260342671239869, 6.723738260341699302 ) ) ;
#1191=DIRECTION ( 'NONE',  ( -1.000000000000000000, 0.000000000000000000, 0.000000000000000000 ) ) ;
#1195=ORIENTED_EDGE ( 'NONE', *, *, #669, .T. ) ;
#1201=EDGE_CURVE ( 'NONE', #4878, #1470, #2683, .T. ) ;
#1205=EDGE_CURVE ( 'NONE', #6074, #1416, #545, .T. ) ;
#1208=DIRECTION ( 'NONE',  ( -0.000000000000000000, -0.000000000000000000, -1.000000000000000000 ) ) ;
#1209=VERTEX_POINT ( 'NONE', #5669 ) ;
#1219=CARTESIAN_POINT ( 'NONE',  ( 0.000000000000000000, 0.000000000000000000, 44.00000000000000711 ) ) ;
#1220=VECTOR ( 'NONE', #5462, 1000.000000000000000 ) ;
#1221=AXIS2_PLACEMENT_3D ( 'NONE', #609, #3557, #4435 ) ;
#1224=CARTESIAN_POINT ( 'NONE',  ( 0.000000000000000000, 25.00000000000000000, 24.27501000028010125 ) ) ;
#1225=AXIS2_PLACEMENT_3D ( 'NONE', #202, #5542, #5061 ) ;
#1226=CARTESIAN_POINT ( 'NONE',  ( 15.99408614349810698, 19.21429697996681796, 0.000000000000000000 ) ) ;
#1227=CARTESIAN_POINT ( 'NONE',  ( 7.059519746509402616, -21.88992045406459042, 34.31748813447425306 ) ) ;
#1231=CARTESIAN_POINT ( 'NONE',  ( 9.185524248261779151E-16, 25.00000000000000000, 39.27501000028010480 ) ) ;
#1239=ORIENTED_EDGE ( 'NONE', *, *, #1593, .T. ) ;
#1242=( NAMED_UNIT ( * ) PLANE_ANGLE_UNIT ( ) SI_UNIT ( $, .RADIAN. ) );
#1243=CARTESIAN_POINT ( 'NONE',  ( -15.23842499831731523, -17.23716120365648052, 1.424676953056493112 ) ) ;
#1258=CARTESIAN_POINT ( 'NONE',  ( 0.000000000000000000, 25.00000000000000000, 31.77501000028010125 ) ) ;
#1262=CARTESIAN_POINT ( 'NONE',  ( 0.000000000000000000, 25.00000000000000000, 31.77501000028010125 ) ) ;
#1275=CARTESIAN_POINT ( 'NONE',  ( -11.95959904370095650, -19.64922365089178768, 5.386438528827848238 ) ) ;
#1283=CARTESIAN_POINT ( 'NONE',  ( -3.337067332043155865, -24.78046181229917266, 25.04046888573288143 ) ) ;
#1287=CARTESIAN_POINT ( 'NONE',  ( 0.9839074788235817604, 24.98539006426129205, 39.22674605012093707 ) ) ;
#1292=CARTESIAN_POINT ( 'NONE',  ( 3.765864371162155333, -24.71817793568963850, 25.27057431607724780 ) ) ;
#1294=VERTEX_POINT ( 'NONE', #6283 ) ;
#1295=CARTESIAN_POINT ( 'NONE',  ( -2.655777422895189144, 24.85958502782042245, 24.75666344040547528 ) ) ;
#1297=CARTESIAN_POINT ( 'NONE',  ( -20.00000000000000000, 0.000000000000000000, 51.00000000000002842 ) ) ;
#1304=CARTESIAN_POINT ( 'NONE',  ( -0.9177768309508191891, -22.98591141273915639, 9.981795115530772478 ) ) ;
#1305=LINE ( 'NONE', #3274, #5136 ) ;
#1307=CARTESIAN_POINT ( 'NONE',  ( 0.000000000000000000, 0.000000000000000000, 47.00000000000000711 ) ) ;
#1314=CARTESIAN_POINT ( 'NONE',  ( -6.734764818747084547, -24.07658780463482984, 35.11236497522016720 ) ) ;
#1316=PRODUCT_DEFINITION_CONTEXT ( 'detailed design', #2911, 'design' ) ;
#1325=CARTESIAN_POINT ( 'NONE',  ( 4.953009495843455845, -24.50520187577543751, 26.13782778128491557 ) ) ;
#1329=CARTESIAN_POINT ( 'NONE',  ( -6.737430854173823036, 24.07581932788625068, 28.44406090190431513 ) ) ;
#1344=AXIS2_PLACEMENT_3D ( 'NONE', #4410, #3020, #6341 ) ;
#1346=VERTEX_POINT ( 'NONE', #524 ) ;
#1347=DIRECTION ( 'NONE',  ( -0.000000000000000000, -0.000000000000000000, -1.000000000000000000 ) ) ;
#1349=CARTESIAN_POINT ( 'NONE',  ( 0.000000000000000000, 25.00000000000000000, 24.27501000028010125 ) ) ;
#1350=AXIS2_PLACEMENT_3D ( 'NONE', #1258, #2764, #2286 ) ;
#1355=CARTESIAN_POINT ( 'NONE',  ( 0.000000000000000000, 0.000000000000000000, 39.00000000000001421 ) ) ;
#1358=CARTESIAN_POINT ( 'NONE',  ( 1.957493960826125923, 24.92801652726308248, 39.03205219918675795 ) ) ;
#1360=CYLINDRICAL_SURFACE ( 'NONE', #1832, 7.500000000000000000 ) ;
#1361=CARTESIAN_POINT ( 'NONE',  ( 6.139315947428367615, -22.16738032098082911, 27.44370026704754650 ) ) ;
#1364=CARTESIAN_POINT ( 'NONE',  ( -4.955340051326917461, 24.50653216723387473, 37.42604413602551716 ) ) ;
#1373=CYLINDRICAL_SURFACE ( 'NONE', #1743, 17.79053956122086078 ) ;
#1377=CARTESIAN_POINT ( 'NONE',  ( -4.240673024049072204, -22.60901396202200075, 25.57291330172528987 ) ) ;
#1385=CARTESIAN_POINT ( 'NONE',  ( 7.018581182383306860, -23.99477090726734829, 29.12000203626550032 ) ) ;
#1386=VERTEX_POINT ( 'NONE', #4959 ) ;
#1388=ORIENTED_EDGE ( 'NONE', *, *, #1436, .F. ) ;
#1392=CARTESIAN_POINT ( 'NONE',  ( 2.012341796004660122, 25.00000000000000000, 39.00000000000001421 ) ) ;
#1393=CARTESIAN_POINT ( 'NONE',  ( -22.00000000000000000, 0.000000000000000000, 50.00000000000000711 ) ) ;
#1397=ORIENTED_EDGE ( 'NONE', *, *, #5347, .T. ) ;
#1399=CARTESIAN_POINT ( 'NONE',  ( 0.000000000000000000, 0.000000000000000000, 44.00000000000000711 ) ) ;
#1400=AXIS2_PLACEMENT_3D ( 'NONE', #5589, #373, #1948 ) ;
#1405=CARTESIAN_POINT ( 'NONE',  ( 6.736323264042102466, -24.07882193050101449, 8.680799421305112062 ) ) ;
#1408=ORIENTED_EDGE ( 'NONE', *, *, #1052, .F. ) ;
#1413=CARTESIAN_POINT ( 'NONE',  ( -0.9006954679665252206, -22.98346407483541753, 24.32584948309267148 ) ) ;
#1414=DIRECTION ( 'NONE',  ( 1.000000000000000000, 0.000000000000000000, 0.000000000000000000 ) ) ;
#1415=DIRECTION ( 'NONE',  ( 0.000000000000000000, 0.000000000000000000, 1.000000000000000000 ) ) ;
#1416=VERTEX_POINT ( 'NONE', #4407 ) ;
#1420=AXIS2_PLACEMENT_3D ( 'NONE', #5660, #3868, #1425 ) ;
#1423=CARTESIAN_POINT ( 'NONE',  ( 1.568280873051609348, -22.94756140746006778, 24.43729500028611312 ) ) ;
#1425=DIRECTION ( 'NONE',  ( -1.000000000000000000, 0.000000000000000000, 0.000000000000000000 ) ) ;
#1429=DIRECTION ( 'NONE',  ( 0.000000000000000000, 0.000000000000000000, -1.000000000000000000 ) ) ;
#1431=CIRCLE ( 'NONE', #5029, 22.00000000000000000 ) ;
#1432=CARTESIAN_POINT ( 'NONE',  ( -2.012341796004660122, 25.00000000000000000, 39.00000000000001421 ) ) ;
#1436=EDGE_CURVE ( 'NONE', #1896, #6074, #5858, .T. ) ;
#1438=LINE ( 'NONE', #1919, #3922 ) ;
#1441=CARTESIAN_POINT ( 'NONE',  ( -9.287558414957933550, -23.21379839259252975, 7.388795739543621899 ) ) ;
#1442=ORIENTED_EDGE ( 'NONE', *, *, #5705, .T. ) ;
#1443=EDGE_CURVE ( 'NONE', #1773, #116, #1861, .T. ) ;
#1450=CYLINDRICAL_SURFACE ( 'NONE', #1961, 7.500000000000000000 ) ;
#1453=CARTESIAN_POINT ( 'NONE',  ( 1.353316873173489032, 19.96515186930334096, 39.18355504947043499 ) ) ;
#1455=VECTOR ( 'NONE', #4398, 1000.000000000000000 ) ;
#1459=CARTESIAN_POINT ( 'NONE',  ( 0.4915545007834231650, -24.99637963107062433, 39.26296923598712851 ) ) ;
#1460=VERTEX_POINT ( 'NONE', #4984 ) ;
#1470=VERTEX_POINT ( 'NONE', #2599 ) ;
#1490=SHAPE_REPRESENTATION ( 'Part 32,2_Varsay\X2\0131\X0\lan', ( #6349 ), #4174 ) ;
#1505=EDGE_LOOP ( 'NONE', ( #2978, #544, #356, #470, #751, #2174 ) ) ;
#1506=AXIS2_PLACEMENT_3D ( 'NONE', #3371, #448, #2343 ) ;
#1508=CARTESIAN_POINT ( 'NONE',  ( -7.267038029898874818, -21.82227126734110456, 29.86717584346564180 ) ) ;
#1511=CARTESIAN_POINT ( 'NONE',  ( -7.182657412981705209E-17, 20.00000000000000711, 39.27501000028011902 ) ) ;
#1521=FACE_OUTER_BOUND ( 'NONE', #2504, .T. ) ;
#1522=EDGE_CURVE ( 'NONE', #3828, #3948, #160, .T. ) ;
#1527=CYLINDRICAL_SURFACE ( 'NONE', #2663, 25.00000000000000000 ) ;
#1530=EDGE_LOOP ( 'NONE', ( #3583, #5534, #2892, #3112, #6191, #6092 ) ) ;
#1536=CARTESIAN_POINT ( 'NONE',  ( -4.673148220383225748, -24.56288069930688067, 9.380541037249376046 ) ) ;
#1541=CARTESIAN_POINT ( 'NONE',  ( -7.071085268539269109, -21.88683845148715079, 34.31457501568616664 ) ) ;
#1548=FACE_OUTER_BOUND ( 'NONE', #3286, .T. ) ;
#1549=CARTESIAN_POINT ( 'NONE',  ( 0.9837646592764097697, -24.98184996318330775, 39.21432222910940624 ) ) ;
#1554=CARTESIAN_POINT ( 'NONE',  ( 5.103812965180195782, 22.42723062334006556, 26.27493091522155666 ) ) ;
#1556=DIRECTION ( 'NONE',  ( 0.000000000000000000, 0.000000000000000000, 1.000000000000000000 ) ) ;
#1560=CARTESIAN_POINT ( 'NONE',  ( 23.00000000000000000, 2.816687638038912352E-15, 0.000000000000000000 ) ) ;
#1562=DIRECTION ( 'NONE',  ( -1.000000000000000000, 0.000000000000000000, 0.000000000000000000 ) ) ;
#1565=PRODUCT_CONTEXT ( 'NONE', #867, 'mechanical' ) ;
#1575=CARTESIAN_POINT ( 'NONE',  ( 11.04889961723839775, 20.18459349909284839, 6.176241220338072324 ) ) ;
#1577=CARTESIAN_POINT ( 'NONE',  ( 3.474965785108256267, 22.73929270720903872, 25.11363447059788712 ) ) ;
#1582=FACE_OUTER_BOUND ( 'NONE', #3616, .T. ) ;
#1593=EDGE_CURVE ( 'NONE', #1416, #6038, #5567, .T. ) ;
#1605=DIRECTION ( 'NONE',  ( -0.000000000000000000, -0.000000000000000000, -1.000000000000000000 ) ) ;
#1606=ORIENTED_EDGE ( 'NONE', *, *, #1443, .F. ) ;
#1608=CARTESIAN_POINT ( 'NONE',  ( -8.270741877429188094, 21.47680860501242961, 7.983294599549966897 ) ) ;
#1610=CARTESIAN_POINT ( 'NONE',  ( 7.058581574212176690, 21.89022081680645826, 29.23014371996821481 ) ) ;
#1611=EDGE_CURVE ( 'NONE', #3765, #394, #5620, .T. ) ;
#1614=CARTESIAN_POINT ( 'NONE',  ( 7.831318214037675141, 23.74511713421663472, 8.189156644668285523 ) ) ;
#1622=AXIS2_PLACEMENT_3D ( 'NONE', #5926, #420, #2374 ) ;
#1629=CARTESIAN_POINT ( 'NONE',  ( -6.710385028064199453, -21.99961506306615178, 35.13225475196805547 ) ) ;
#1632=AXIS2_PLACEMENT_3D ( 'NONE', #2787, #2984, #1562 ) ;
#1633=CYLINDRICAL_SURFACE ( 'NONE', #5777, 7.500000000000000000 ) ;
#1644=CARTESIAN_POINT ( 'NONE',  ( -14.34541152806172626, 17.98734769216428830, 2.761683449857409656 ) ) ;
#1645=CARTESIAN_POINT ( 'NONE',  ( 7.460990961498263019, 21.75625611239105694, 30.97809455494030928 ) ) ;
#1656=CARTESIAN_POINT ( 'NONE',  ( -20.00000000000000000, 0.000000000000000000, 51.00000000000002842 ) ) ;
#1667=ADVANCED_FACE ( 'NONE', ( #1582 ), #1164, .F. ) ;
#1668=LINE ( 'NONE', #6090, #3986 ) ;
#1674=CARTESIAN_POINT ( 'NONE',  ( -6.978968890507021960, 21.91580918028467195, 29.01915572147083822 ) ) ;
#1679=VERTEX_POINT ( 'NONE', #1560 ) ;
#1683=DIRECTION ( 'NONE',  ( 0.000000000000000000, 0.000000000000000000, 1.000000000000000000 ) ) ;
#1685=CARTESIAN_POINT ( 'NONE',  ( -14.33006727100666033, -20.49285708348135415, 2.782958588747959983 ) ) ;
#1697=CARTESIAN_POINT ( 'NONE',  ( 1.908796811648538206E-15, -20.00000000000000711, 39.27501000028011902 ) ) ;
#1707=EDGE_CURVE ( 'NONE', #2247, #3626, #3138, .T. ) ;
#1709=CARTESIAN_POINT ( 'NONE',  ( -1.231226070028328401, 24.97084192177787543, 39.17738101704807718 ) ) ;
#1713=DIRECTION ( 'NONE',  ( 0.000000000000000000, 0.000000000000000000, -1.000000000000000000 ) ) ;
#1724=CARTESIAN_POINT ( 'NONE',  ( -23.00000000000000000, 0.000000000000000000, 39.00000000000001421 ) ) ;
#1728=ORIENTED_EDGE ( 'NONE', *, *, #4345, .F. ) ;
#1740=CARTESIAN_POINT ( 'NONE',  ( -12.81154844869972997, 19.11229287055882864, 4.578663348692236568 ) ) ;
#1741=AXIS2_PLACEMENT_3D ( 'NONE', #4620, #2682, #1713 ) ;
#1743=AXIS2_PLACEMENT_3D ( 'NONE', #2403, #869, #5767 ) ;
#1751=ORIENTED_EDGE ( 'NONE', *, *, #1707, .F. ) ;
#1752=AXIS2_PLACEMENT_3D ( 'NONE', #2533, #1415, #3508 ) ;
#1764=CARTESIAN_POINT ( 'NONE',  ( 15.23263781889692048, -17.24245498722747527, 1.434805278142651241 ) ) ;
#1772=CARTESIAN_POINT ( 'NONE',  ( -7.451677332883843263, -23.86383568307784131, 30.79254100948602613 ) ) ;
#1773=VERTEX_POINT ( 'NONE', #732 ) ;
#1779=CARTESIAN_POINT ( 'NONE',  ( 5.578949544899560742, -22.31500106593816213, 26.74243945601464745 ) ) ;
#1782=CARTESIAN_POINT ( 'NONE',  ( -5.133479616427195857, 24.46790356832289248, 26.30175839968468665 ) ) ;
#1801=EDGE_CURVE ( 'NONE', #959, #2940, #3767, .T. ) ;
#1802=DIRECTION ( 'NONE',  ( 0.000000000000000000, 0.000000000000000000, -1.000000000000000000 ) ) ;
#1803=LINE ( 'NONE', #5776, #2531 ) ;
#1810=CARTESIAN_POINT ( 'NONE',  ( -1.353091841878392376, 19.95700839110197933, 39.15972426387312311 ) ) ;
#1811=LINE ( 'NONE', #1224, #3738 ) ;
#1815=CARTESIAN_POINT ( 'NONE',  ( 7.491878387983184062, -21.74571065617575982, 31.20484628725278498 ) ) ;
#1816=VERTEX_POINT ( 'NONE', #4971 ) ;
#1830=LINE ( 'NONE', #6183, #5979 ) ;
#1832=AXIS2_PLACEMENT_3D ( 'NONE', #1262, #2860, #852 ) ;
#1836=CARTESIAN_POINT ( 'NONE',  ( 0.000000000000000000, 0.000000000000000000, 41.00000000000000000 ) ) ;
#1839=CARTESIAN_POINT ( 'NONE',  ( -5.641746473127986938, -24.35561814371765266, 36.72278580929200587 ) ) ;
#1840=ORIENTED_EDGE ( 'NONE', *, *, #5629, .T. ) ;
#1842=CARTESIAN_POINT ( 'NONE',  ( 5.475713916123539526, 24.39360375241167134, 36.90593746307732204 ) ) ;
#1844=CIRCLE ( 'NONE', #3580, 25.00000000000000000 ) ;
#1845=ADVANCED_FACE ( 'NONE', ( #1521 ), #3907, .T. ) ;
#1846=DIRECTION ( 'NONE',  ( 1.000000000000000000, 0.000000000000000000, 0.000000000000000000 ) ) ;
#1847=CARTESIAN_POINT ( 'NONE',  ( 2.421623179306582330, -24.88356973210974843, 24.67241923065279607 ) ) ;
#1853=CARTESIAN_POINT ( 'NONE',  ( -6.367429986337528547, 24.17592611763979704, 35.74554154416229323 ) ) ;
#1854=AXIS2_PLACEMENT_3D ( 'NONE', #2040, #1556, #599 ) ;
#1856=LINE ( 'NONE', #1393, #4206 ) ;
#1861=B_SPLINE_CURVE_WITH_KNOTS ( 'NONE', 3,
 ( #5961, #92, #2624, #4066 ),
 .UNSPECIFIED., .F., .F.,
 ( 4, 4 ),
 ( 0.000000000000000000, 0.002032958594636734458 ),
 .UNSPECIFIED. ) ;
#1869=LINE ( 'NONE', #1349, #2329 ) ;
#1873=CARTESIAN_POINT ( 'NONE',  ( -6.097143767825691008, -24.24550159253069026, 36.14924867743861370 ) ) ;
#1880=CARTESIAN_POINT ( 'NONE',  ( 6.724622458085284471, -24.07890901287614227, 35.10508533856562252 ) ) ;
#1895=CARTESIAN_POINT ( 'NONE',  ( 12.78450670028659886, -21.48642263404485320, 4.587769495204018888 ) ) ;
#1896=VERTEX_POINT ( 'NONE', #3388 ) ;
#1898=CARTESIAN_POINT ( 'NONE',  ( -7.481756639719942648, -21.74910199390652465, 31.20551891105749931 ) ) ;
#1900=CARTESIAN_POINT ( 'NONE',  ( -0.9839074788235784297, -24.98539006426129561, 39.22674605012092997 ) ) ;
#1903=DIRECTION ( 'NONE',  ( 0.000000000000000000, 0.000000000000000000, 1.000000000000000000 ) ) ;
#1905=CARTESIAN_POINT ( 'NONE',  ( 6.367429986337532988, -24.17592611763979704, 35.74554154416227192 ) ) ;
#1909=ORIENTED_EDGE ( 'NONE', *, *, #5738, .F. ) ;
#1910=CARTESIAN_POINT ( 'NONE',  ( -6.135028333862784677, 22.16704433745741554, 36.09490741883096376 ) ) ;
#1911=EDGE_CURVE ( 'NONE', #2192, #4936, #2298, .T. ) ;
#1913=EDGE_CURVE ( 'NONE', #4936, #635, #6073, .T. ) ;
#1919=CARTESIAN_POINT ( 'NONE',  ( 22.00000000000000000, 2.694222958124176809E-15, 44.00000000000000711 ) ) ;
#1936=AXIS2_PLACEMENT_3D ( 'NONE', #4281, #3808, #5196 ) ;
#1939=DIRECTION ( 'NONE',  ( 1.000000000000000000, 0.000000000000000000, -0.000000000000000000 ) ) ;
#1940=AXIS2_PLACEMENT_3D ( 'NONE', #3842, #2866, #4349 ) ;
#1943=ORIENTED_EDGE ( 'NONE', *, *, #3209, .F. ) ;
#1944=CARTESIAN_POINT ( 'NONE',  ( 23.00000000000000000, 2.816687638038912352E-15, 39.00000000000001421 ) ) ;
#1948=DIRECTION ( 'NONE',  ( 1.000000000000000000, 0.000000000000000000, 0.000000000000000000 ) ) ;
#1956=FACE_OUTER_BOUND ( 'NONE', #872, .T. ) ;
#1961=AXIS2_PLACEMENT_3D ( 'NONE', #4960, #4467, #5387 ) ;
#1963=CARTESIAN_POINT ( 'NONE',  ( -6.802364521716127044, -21.97126452515143313, 28.60827024242000149 ) ) ;
#1973=CARTESIAN_POINT ( 'NONE',  ( 0.4985038669289038604, 25.00000000000000000, 24.27501000028010480 ) ) ;
#1975=AXIS2_PLACEMENT_3D ( 'NONE', #5093, #3455, #6119 ) ;
#1978=CARTESIAN_POINT ( 'NONE',  ( 3.536994606882255532, 22.74309932279132340, 9.666805580179055113 ) ) ;
#1979=ORIENTED_EDGE ( 'NONE', *, *, #2532, .F. ) ;
#1983=CARTESIAN_POINT ( 'NONE',  ( -15.99408614349810698, 25.00000000000000000, -4.336808689942017736E-15 ) ) ;
#1986=ORIENTED_EDGE ( 'NONE', *, *, #2769, .F. ) ;
#1990=CARTESIAN_POINT ( 'NONE',  ( 11.91160812950988124, -21.98255961136171877, 5.429893957167271523 ) ) ;
#1994=PLANE ( 'NONE',  #1344 ) ;
#1996=EDGE_CURVE ( 'NONE', #1896, #1020, #1811, .T. ) ;
#2001=CARTESIAN_POINT ( 'NONE',  ( 0.000000000000000000, 0.000000000000000000, 0.000000000000000000 ) ) ;
#2012=ORIENTED_EDGE ( 'NONE', *, *, #4103, .T. ) ;
#2014=ORIENTED_EDGE ( 'NONE', *, *, #5278, .F. ) ;
#2015=LINE ( 'NONE', #54, #5517 ) ;
#2025=AXIS2_PLACEMENT_3D ( 'NONE', #3027, #3988, #5969 ) ;
#2029=EDGE_LOOP ( 'NONE', ( #481, #706, #440, #1979, #1751, #4429 ) ) ;
#2033=CARTESIAN_POINT ( 'NONE',  ( 1.231226070028332398, -24.97084192177786832, 39.17738101704806297 ) ) ;
#2037=CARTESIAN_POINT ( 'NONE',  ( -5.269070065585171214, 22.39093555978999817, 26.41927588677976502 ) ) ;
#2038=AXIS2_PLACEMENT_3D ( 'NONE', #2001, #3381, #586 ) ;
#2039=CARTESIAN_POINT ( 'NONE',  ( -22.00000000000000000, 0.000000000000000000, 44.00000000000000711 ) ) ;
#2040=CARTESIAN_POINT ( 'NONE',  ( 0.000000000000000000, 0.000000000000000000, 50.00000000000000711 ) ) ;
#2042=EDGE_LOOP ( 'NONE', ( #5382, #6214 ) ) ;
#2047=CARTESIAN_POINT ( 'NONE',  ( 20.00000000000000000, 2.449293598294706513E-15, 51.00000000000002842 ) ) ;
#2055=CARTESIAN_POINT ( 'NONE',  ( -5.735021534702854140, -22.27575375288411408, 36.62858606677772144 ) ) ;
#2061=AXIS2_PLACEMENT_3D ( 'NONE', #4763, #1347, #355 ) ;
#2063=CARTESIAN_POINT ( 'NONE',  ( 15.99408614349810698, 19.21429697996681796, 0.000000000000000000 ) ) ;
#2068=CARTESIAN_POINT ( 'NONE',  ( 0.4497881292104084494, 22.99670767401471849, 24.28508774596658526 ) ) ;
#2072=ORIENTED_EDGE ( 'NONE', *, *, #2303, .T. ) ;
#2081=EDGE_CURVE ( 'NONE', #4602, #3869, #141, .T. ) ;
#2086=CARTESIAN_POINT ( 'NONE',  ( -3.680439676527237136, -22.70725644061459647, 38.32515107347151684 ) ) ;
#2089=ORIENTED_EDGE ( 'NONE', *, *, #1611, .T. ) ;
#2090=DIRECTION ( 'NONE',  ( -1.000000000000000000, 0.000000000000000000, 0.000000000000000000 ) ) ;
#2094=CARTESIAN_POINT ( 'NONE',  ( 8.336125322366124024, 21.45114114349586387, 7.948328953041721157 ) ) ;
#2095=CARTESIAN_POINT ( 'NONE',  ( -2.436617367782499599, 22.87153588547686667, 24.67833651202806067 ) ) ;
#2096=CARTESIAN_POINT ( 'NONE',  ( 2.985931097914281462, 24.82479382442820537, 9.752995572818681680 ) ) ;
#2100=ORIENTED_EDGE ( 'NONE', *, *, #1443, .T. ) ;
#2106=PLANE ( 'NONE',  #900 ) ;
#2117=ADVANCED_FACE ( 'NONE', ( #4343 ), #2962, .T. ) ;
#2118=DIRECTION ( 'NONE',  ( -0.000000000000000000, -0.000000000000000000, -1.000000000000000000 ) ) ;
#2121=CARTESIAN_POINT ( 'NONE',  ( 0.000000000000000000, 0.000000000000000000, 39.00000000000001421 ) ) ;
#2124=AXIS2_PLACEMENT_3D ( 'NONE', #641, #451, #1414 ) ;
#2125=CYLINDRICAL_SURFACE ( 'NONE', #4409, 25.00000000000000000 ) ;
#2126=CARTESIAN_POINT ( 'NONE',  ( 2.226229255992760780, 22.89589894665499870, 24.59902000234163211 ) ) ;
#2127=CARTESIAN_POINT ( 'NONE',  ( -8.983986218495344289, 23.34169575125378771, 7.586426789398493575 ) ) ;
#2131=CIRCLE ( 'NONE', #6050, 23.00000000000000000 ) ;
#2132=CARTESIAN_POINT ( 'NONE',  ( 0.000000000000000000, 0.000000000000000000, 51.00000000000002842 ) ) ;
#2136=CARTESIAN_POINT ( 'NONE',  ( 0.000000000000000000, 0.000000000000000000, 47.00000000000000711 ) ) ;
#2142=DIRECTION ( 'NONE',  ( -0.000000000000000000, 1.000000000000000000, -0.000000000000000000 ) ) ;
#2151=DIRECTION ( 'NONE',  ( -0.000000000000000000, -0.000000000000000000, -1.000000000000000000 ) ) ;
#2157=CARTESIAN_POINT ( 'NONE',  ( 1.127325861074953917, 22.97343572093476638, 24.35677350376877470 ) ) ;
#2159=CARTESIAN_POINT ( 'NONE',  ( -7.127827911436782848, 23.96564785266029673, 8.515057432034145890 ) ) ;
#2162=CARTESIAN_POINT ( 'NONE',  ( 6.002163747819661666, -22.20348677930560655, 36.27767814654681899 ) ) ;
#2172=( NAMED_UNIT ( * ) SI_UNIT ( $, .STERADIAN. ) SOLID_ANGLE_UNIT ( ) );
#2173=CARTESIAN_POINT ( 'NONE',  ( -6.810998761473115337, -21.97232263399875762, 8.650160397932937784 ) ) ;
#2174=ORIENTED_EDGE ( 'NONE', *, *, #4687, .T. ) ;
#2175=CARTESIAN_POINT ( 'NONE',  ( 0.000000000000000000, 25.00000000000000000, 31.77501000028010125 ) ) ;
#2183=EDGE_LOOP ( 'NONE', ( #3037, #511 ) ) ;
#2192=VERTEX_POINT ( 'NONE', #5391 ) ;
#2204=( LENGTH_UNIT ( ) NAMED_UNIT ( * ) SI_UNIT ( .MILLI., .METRE. ) );
#2205=CARTESIAN_POINT ( 'NONE',  ( 12.81154844869972997, -19.11229287055882864, 4.578663348692236568 ) ) ;
#2209=VECTOR ( 'NONE', #2142, 1000.000000000000000 ) ;
#2215=CARTESIAN_POINT ( 'NONE',  ( 2.239119884489100709, 22.89489171314753335, 9.863953455948397675 ) ) ;
#2222=CARTESIAN_POINT ( 'NONE',  ( 6.505027467542590536, -22.06241888168487009, 35.53465933272089927 ) ) ;
#2225=CARTESIAN_POINT ( 'NONE',  ( -6.724622458085280918, 24.07890901287612806, 35.10508533856560831 ) ) ;
#2235=CARTESIAN_POINT ( 'NONE',  ( 15.99408614349810698, -16.52843635781563592, 0.000000000000000000 ) ) ;
#2236=CARTESIAN_POINT ( 'NONE',  ( 13.86188709689055543, -18.36473791091104246, 3.388952392393740354 ) ) ;
#2242=DIRECTION ( 'NONE',  ( 0.000000000000000000, 0.000000000000000000, 1.000000000000000000 ) ) ;
#2245=CARTESIAN_POINT ( 'NONE',  ( 0.000000000000000000, 0.000000000000000000, 55.00000000000000711 ) ) ;
#2246=CARTESIAN_POINT ( 'NONE',  ( -7.114947004179562384, -23.96699118800356842, 34.19833922271499915 ) ) ;
#2247=VERTEX_POINT ( 'NONE', #4313 ) ;
#2250=AXIS2_PLACEMENT_3D ( 'NONE', #243, #1683, #5176 ) ;
#2255=CARTESIAN_POINT ( 'NONE',  ( 1.790150932673403750, -22.93126094008908566, 24.48831024192238814 ) ) ;
#2260=CARTESIAN_POINT ( 'NONE',  ( -3.769188925537567236, 24.71764851934220530, 38.27740560533011660 ) ) ;
#2266=ORIENTED_EDGE ( 'NONE', *, *, #3209, .T. ) ;
#2273=CARTESIAN_POINT ( 'NONE',  ( -2.239119884489100709, -22.89489171314753335, 9.863953455948397675 ) ) ;
#2274=EDGE_LOOP ( 'NONE', ( #5039, #5820, #4176, #878, #6063, #4442 ) ) ;
#2282=CARTESIAN_POINT ( 'NONE',  ( -5.952041157299176710, -24.28165242506072019, 36.34480154750762892 ) ) ;
#2283=EDGE_LOOP ( 'NONE', ( #6128, #4516, #5663 ) ) ;
#2286=DIRECTION ( 'NONE',  ( 0.000000000000000000, 0.000000000000000000, -1.000000000000000000 ) ) ;
#2290=CARTESIAN_POINT ( 'NONE',  ( 6.096488593930911470, -24.24566755320544686, 36.15017996222949392 ) ) ;
#2293=CARTESIAN_POINT ( 'NONE',  ( -7.257770128441432433, 23.92352318576052284, 33.72861583961352494 ) ) ;
#2294=EDGE_CURVE ( 'NONE', #3869, #12, #4988, .T. ) ;
#2298=B_SPLINE_CURVE_WITH_KNOTS ( 'NONE', 3,
 ( #4939, #4873, #462, #915, #3420, #2869, #5459, #2491, #3968, #1040, #435, #4352, #1910, #3870, #5849, #953, #2422, #4996, #1158, #2610, #627, #3609, #143, #4571, #174, #5581, #1674, #5099, #4509, #563, #4538, #3575, #2037, #5608, #4479, #207, #2517, #2095, #4048, #1186, #3123, #3993, #75, #6096 ),
 .UNSPECIFIED., .F., .F.,
 ( 4, 2, 2, 2, 2, 2, 2, 2, 2, 2, 2, 2, 2, 2, 2, 2, 2, 2, 2, 2, 2, 4 ),
 ( 0.000000000000000000, 0.001348713335717714561, 0.002023070003576572708, 0.002697426671435430422, 0.004046140007153132406, 0.004720496675011990988, 0.005394853342870850436, 0.006743566678588568467, 0.007417923346447437456, 0.008092280014306306446, 0.009440993350024065242, 0.01078970668574182230, 0.01213842002145957069, 0.01281277668931844402, 0.01348713335717731908, 0.01483584669289507441, 0.01618456002861283147, 0.01753327336433058506, 0.01888198670004834212, 0.01955634336790721892, 0.02023070003576609918, 0.02157941337148385624 ),
 .UNSPECIFIED. ) ;
#2302=EDGE_CURVE ( 'NONE', #1416, #2192, #3967, .T. ) ;
#2303=EDGE_CURVE ( 'NONE', #2192, #3708, #5451, .T. ) ;
#2306=ORIENTED_EDGE ( 'NONE', *, *, #4687, .F. ) ;
#2307=DIRECTION ( 'NONE',  ( 0.000000000000000000, 0.000000000000000000, 1.000000000000000000 ) ) ;
#2316=CARTESIAN_POINT ( 'NONE',  ( -7.307255365082233389, -23.90829471491151281, 30.06775954199971679 ) ) ;
#2317=ORIENTED_EDGE ( 'NONE', *, *, #5618, .F. ) ;
#2324=CARTESIAN_POINT ( 'NONE',  ( 6.493108461366341899, -24.14236833790515036, 35.53659098058280108 ) ) ;
#2327=CARTESIAN_POINT ( 'NONE',  ( -7.115105366545458665, 23.96693872413611004, 34.19760250332532081 ) ) ;
#2329=VECTOR ( 'NONE', #3830, 1000.000000000000000 ) ;
#2330=DIRECTION ( 'NONE',  ( -0.000000000000000000, 1.000000000000000000, -0.000000000000000000 ) ) ;
#2337=DIRECTION ( 'NONE',  ( -1.000000000000000000, 0.000000000000000000, 0.000000000000000000 ) ) ;
#2343=DIRECTION ( 'NONE',  ( -1.000000000000000000, 0.000000000000000000, 0.000000000000000000 ) ) ;
#2344=CARTESIAN_POINT ( 'NONE',  ( 0.000000000000000000, 0.000000000000000000, 39.00000000000001421 ) ) ;
#2347=CARTESIAN_POINT ( 'NONE',  ( -1.957493960826122814, -24.92801652726308248, 39.03205219918674374 ) ) ;
#2350=CARTESIAN_POINT ( 'NONE',  ( 3.769534566620170057, 24.71760338780762822, 38.27724873576354980 ) ) ;
#2356=CIRCLE ( 'NONE', #2466, 40.00000002749906258 ) ;
#2357=CARTESIAN_POINT ( 'NONE',  ( 7.499773188859401252, -23.84855136421925081, 31.27916535100970563 ) ) ;
#2364=LINE ( 'NONE', #1392, #690 ) ;
#2366=DIRECTION ( 'NONE',  ( 0.000000000000000000, -1.000000000000000000, 0.000000000000000000 ) ) ;
#2372=DIRECTION ( 'NONE',  ( -1.000000000000000000, 0.000000000000000000, 0.000000000000000000 ) ) ;
#2374=DIRECTION ( 'NONE',  ( 1.000000000000000000, 0.000000000000000000, -0.000000000000000000 ) ) ;
#2376=CARTESIAN_POINT ( 'NONE',  ( -5.722301980643075048, -22.27724803853372393, 26.92170784547232998 ) ) ;
#2380=CARTESIAN_POINT ( 'NONE',  ( -4.956647734651107307, -24.50626513604597889, 37.42488445140200071 ) ) ;
#2382=DIRECTION ( 'NONE',  ( -1.000000000000000000, 0.000000000000000000, 0.000000000000000000 ) ) ;
#2387=CARTESIAN_POINT ( 'NONE',  ( 1.948881123199609489, -24.92505092879369499, 24.52843033598425393 ) ) ;
#2396=CARTESIAN_POINT ( 'NONE',  ( -25.00000000000000000, 0.000000000000000000, 41.00000000000000000 ) ) ;
#2403=CARTESIAN_POINT ( 'NONE',  ( 0.000000000000000000, 25.00000000000000000, -7.790539539321167162 ) ) ;
#2410=CARTESIAN_POINT ( 'NONE',  ( -5.266685217916866613, -22.38944685319058436, 26.43066030061579141 ) ) ;
#2413=ORIENTED_EDGE ( 'NONE', *, *, #4360, .T. ) ;
#2414=CARTESIAN_POINT ( 'NONE',  ( 9.184177739184520255E-16, -25.00000000000000000, 39.27501000028010480 ) ) ;
#2422=CARTESIAN_POINT ( 'NONE',  ( -7.059519746509402616, 21.88992045406459042, 34.31748813447425306 ) ) ;
#2429=ORIENTED_EDGE ( 'NONE', *, *, #5467, .T. ) ;
#2433=DIRECTION ( 'NONE',  ( -0.000000000000000000, -0.000000000000000000, -1.000000000000000000 ) ) ;
#2434=FACE_OUTER_BOUND ( 'NONE', #2515, .T. ) ;
#2437=( LENGTH_UNIT ( ) NAMED_UNIT ( * ) SI_UNIT ( .MILLI., .METRE. ) );
#2441=ORIENTED_EDGE ( 'NONE', *, *, #2302, .F. ) ;
#2445=CARTESIAN_POINT ( 'NONE',  ( 5.649026277996902046, 24.35594688685564790, 26.81770774654597034 ) ) ;
#2448=CARTESIAN_POINT ( 'NONE',  ( 0.2456693407522394235, -24.99999999999999645, 39.27501000028009770 ) ) ;
#2450=CARTESIAN_POINT ( 'NONE',  ( 4.378668635177231927, 22.59503479412315485, 9.474032806803469597 ) ) ;
#2463=DIRECTION ( 'NONE',  ( -1.000000000000000000, 0.000000000000000000, 0.000000000000000000 ) ) ;
#2466=AXIS2_PLACEMENT_3D ( 'NONE', #5487, #2550, #113 ) ;
#2468=CARTESIAN_POINT ( 'NONE',  ( 14.34088693563092853, -20.48519421429849174, 2.767956487184815462 ) ) ;
#2470=ORIENTED_EDGE ( 'NONE', *, *, #264, .F. ) ;
#2471=AXIS2_PLACEMENT_3D ( 'NONE', #4207, #2307, #252 ) ;
#2482=CARTESIAN_POINT ( 'NONE',  ( 4.574685241957344495, 24.57863749249463936, 25.82670804586578228 ) ) ;
#2484=PLANE ( 'NONE',  #2038 ) ;
#2485=AXIS2_PLACEMENT_3D ( 'NONE', #1836, #359, #2821 ) ;
#2491=CARTESIAN_POINT ( 'NONE',  ( -4.782950468712823699, 22.50022147858462418, 37.56939778472803226 ) ) ;
#2503=CARTESIAN_POINT ( 'NONE',  ( -8.206466222643920005, -23.61787042823059224, 7.999630148859495193 ) ) ;
#2504=EDGE_LOOP ( 'NONE', ( #3300, #404, #832, #5496 ) ) ;
#2515=EDGE_LOOP ( 'NONE', ( #4366, #4186 ) ) ;
#2517=CARTESIAN_POINT ( 'NONE',  ( -3.063555513103408678, 22.79893987554409662, 24.91467890029023025 ) ) ;
#2531=VECTOR ( 'NONE', #392, 1000.000000000000000 ) ;
#2532=EDGE_CURVE ( 'NONE', #3626, #3948, #5729, .T. ) ;
#2533=CARTESIAN_POINT ( 'NONE',  ( 0.000000000000000000, 0.000000000000000000, 44.00000000000000711 ) ) ;
#2543=CARTESIAN_POINT ( 'NONE',  ( 13.09536939405042055, 18.91069771112636744, 4.258167217702273355 ) ) ;
#2545=DIRECTION ( 'NONE',  ( 1.000000000000000000, 0.000000000000000000, 0.000000000000000000 ) ) ;
#2546=CARTESIAN_POINT ( 'NONE',  ( 7.267038029898874818, 21.82227126734110456, 29.86717584346564180 ) ) ;
#2550=DIRECTION ( 'NONE',  ( 0.000000000000000000, -1.000000000000000000, 0.000000000000000000 ) ) ;
#2576=CARTESIAN_POINT ( 'NONE',  ( 12.25547752887834818, 19.46581264560981239, 5.111654144181065895 ) ) ;
#2579=CARTESIAN_POINT ( 'NONE',  ( 7.412736743525290883, 21.77298136741688950, 33.00284858769864371 ) ) ;
#2580=CARTESIAN_POINT ( 'NONE',  ( -11.91160812950987946, 21.98255961136171877, 5.429893957167271523 ) ) ;
#2582=EDGE_CURVE ( 'NONE', #959, #4936, #1869, .T. ) ;
#2593=B_SPLINE_CURVE_WITH_KNOTS ( 'NONE', 3,
 ( #6126, #4084, #5582, #629, #4672, #210, #4572, #1092, #2580, #2640, #3640, #2127, #2674, #2159, #3124, #176, #4118, #6097, #5100, #4539, #2701, #5609, #6070, #758, #144, #2096, #3577, #2611, #3673, #3097, #4049, #1614, #5034, #3067, #692, #1189, #265, #3158, #5647, #6158, #5550, #5130, #4182, #4642, #5067, #1226 ),
 .UNSPECIFIED., .F., .F.,
 ( 4, 2, 2, 2, 2, 2, 2, 2, 2, 2, 2, 2, 2, 2, 2, 2, 2, 2, 2, 2, 2, 2, 4 ),
 ( 4.230440722825154659E-18, 0.002589099528182561144, 0.005178199056365117951, 0.006472748820456394186, 0.007767298584547670422, 0.01035639811273022376, 0.01294549764091277796, 0.01424004740500405854, 0.01553459716909533911, 0.01812369669727790025, 0.01941824646136917909, 0.02071279622546045793, 0.02330189575364301907, 0.02459644551773429791, 0.02589099528182557675, 0.02848009481000812748, 0.02977464457409940632, 0.03106919433819068516, 0.03365829386637324283, 0.03495284363046452514, 0.03624739339455580051, 0.03883649292273835818, 0.04142559245092091585 ),
 .UNSPECIFIED. ) ;
#2599=CARTESIAN_POINT ( 'NONE',  ( 25.00000000000000000, 3.061616997868383043E-15, 41.00000000000000000 ) ) ;
#2602=ORIENTED_EDGE ( 'NONE', *, *, #1911, .T. ) ;
#2608=CARTESIAN_POINT ( 'NONE',  ( -4.711348314259845793, 22.51623045471248119, 9.370182291681606657 ) ) ;
#2610=CARTESIAN_POINT ( 'NONE',  ( -7.411490251847205002, 21.77340291014862217, 33.00915547857365340 ) ) ;
#2611=CARTESIAN_POINT ( 'NONE',  ( 4.258741324358275904, 24.63828325354172222, 9.488137494773077663 ) ) ;
#2612=CARTESIAN_POINT ( 'NONE',  ( 0.000000000000000000, 0.000000000000000000, 0.000000000000000000 ) ) ;
#2624=CARTESIAN_POINT ( 'NONE',  ( -0.6825543444542548910, -20.00000000000000000, 39.27501000028010480 ) ) ;
#2629=AXIS2_PLACEMENT_3D ( 'NONE', #437, #1429, #5372 ) ;
#2632=CARTESIAN_POINT ( 'NONE',  ( 25.00000000000000000, 3.061616997868383043E-15, 44.00000000000000711 ) ) ;
#2634=FACE_OUTER_BOUND ( 'NONE', #1530, .T. ) ;
#2638=CARTESIAN_POINT ( 'NONE',  ( 6.011784583892834100, 22.20189362571451142, 36.28151155367954317 ) ) ;
#2640=CARTESIAN_POINT ( 'NONE',  ( -10.99369682877389209, 22.46365890119679065, 6.219949983291193085 ) ) ;
#2645=AXIS2_PLACEMENT_3D ( 'NONE', #3290, #5230, #4803 ) ;
#2646=CARTESIAN_POINT ( 'NONE',  ( 0.000000000000000000, 0.000000000000000000, 39.00000000000001421 ) ) ;
#2657=ORIENTED_EDGE ( 'NONE', *, *, #3608, .F. ) ;
#2663=AXIS2_PLACEMENT_3D ( 'NONE', #4944, #3550, #4513 ) ;
#2670=DIRECTION ( 'NONE',  ( 1.224646799147353207E-16, 1.000000000000000000, -0.000000000000000000 ) ) ;
#2674=CARTESIAN_POINT ( 'NONE',  ( -8.266016972479206970, 23.60732501453303200, 7.985288904279078892 ) ) ;
#2682=DIRECTION ( 'NONE',  ( 0.000000000000000000, -1.000000000000000000, 0.000000000000000000 ) ) ;
#2683=CIRCLE ( 'NONE', #2485, 25.00000000000000000 ) ;
#2687=CARTESIAN_POINT ( 'NONE',  ( 12.24406280880444164, -19.48300239097275721, 5.141666792244760309 ) ) ;
#2695=FACE_OUTER_BOUND ( 'NONE', #5882, .T. ) ;
#2697=FACE_OUTER_BOUND ( 'NONE', #6143, .T. ) ;
#2701=CARTESIAN_POINT ( 'NONE',  ( -1.764366888834147495, 24.94145795391612808, 9.917654830493177087 ) ) ;
#2705=CARTESIAN_POINT ( 'NONE',  ( -5.958341177435922731, 24.28123298992124290, 27.19342269918142563 ) ) ;
#2714=CARTESIAN_POINT ( 'NONE',  ( 8.270741877429188094, -21.47680860501242961, 7.983294599549966897 ) ) ;
#2715=EDGE_LOOP ( 'NONE', ( #1986, #3776, #3494, #4205, #3644, #2306, #1177 ) ) ;
#2716=DIRECTION ( 'NONE',  ( 0.000000000000000000, 0.000000000000000000, 1.000000000000000000 ) ) ;
#2727=CARTESIAN_POINT ( 'NONE',  ( 7.487557334333944326, 23.85240338065036880, 32.27275042597646149 ) ) ;
#2730=ADVANCED_FACE ( 'NONE', ( #736 ), #219, .F. ) ;
#2737=CARTESIAN_POINT ( 'NONE',  ( -7.500225230914492336, 23.84840920358613303, 32.26396939133217501 ) ) ;
#2739=EDGE_CURVE ( 'NONE', #3765, #6038, #209, .T. ) ;
#2741=CARTESIAN_POINT ( 'NONE',  ( 0.000000000000000000, 0.000000000000000000, 23.77500997278103512 ) ) ;
#2749=CARTESIAN_POINT ( 'NONE',  ( -7.200995294576264527, -21.84734027758491237, 8.482870732638906119 ) ) ;
#2762=ORIENTED_EDGE ( 'NONE', *, *, #4874, .F. ) ;
#2764=DIRECTION ( 'NONE',  ( 0.000000000000000000, -1.000000000000000000, 0.000000000000000000 ) ) ;
#2768=CARTESIAN_POINT ( 'NONE',  ( 7.115105366545459553, -23.96693872413611004, 34.19760250332532081 ) ) ;
#2769=EDGE_CURVE ( 'NONE', #5038, #3626, #3723, .T. ) ;
#2773=CARTESIAN_POINT ( 'NONE',  ( -5.951225761847359408, 24.28185285436555674, 36.34586759703542214 ) ) ;
#2781=AXIS2_PLACEMENT_3D ( 'NONE', #1005, #2963, #1939 ) ;
#2786=CARTESIAN_POINT ( 'NONE',  ( 6.736606839469455821, -22.00628563274161920, 8.696944893850881542 ) ) ;
#2787=CARTESIAN_POINT ( 'NONE',  ( 0.000000000000000000, 0.000000000000000000, 51.00000000000002842 ) ) ;
#2793=ORIENTED_EDGE ( 'NONE', *, *, #5278, .T. ) ;
#2795=EDGE_CURVE ( 'NONE', #3396, #1816, #3079, .T. ) ;
#2798=CARTESIAN_POINT ( 'NONE',  ( -4.574685241957346271, -24.57863749249464291, 25.82670804586579294 ) ) ;
#2802=CARTESIAN_POINT ( 'NONE',  ( -0.3392246580399966294, 19.99999999999999645, 39.27501000028010480 ) ) ;
#2806=CARTESIAN_POINT ( 'NONE',  ( 2.436617367782499599, -22.87153588547686667, 24.67833651202806067 ) ) ;
#2809=CARTESIAN_POINT ( 'NONE',  ( -7.018581182383311301, 23.99477090726735895, 29.12000203626552164 ) ) ;
#2813=CARTESIAN_POINT ( 'NONE',  ( 9.185524248261779151E-16, 25.00000000000000000, 39.27501000028010480 ) ) ;
#2821=DIRECTION ( 'NONE',  ( 1.000000000000000000, 0.000000000000000000, 0.000000000000000000 ) ) ;
#2822=CARTESIAN_POINT ( 'NONE',  ( -2.012341796004660122, -22.91179784512888773, 39.00000000000001421 ) ) ;
#2823=CARTESIAN_POINT ( 'NONE',  ( -7.102515314070984687, -23.96997983984567782, 29.35314634237168718 ) ) ;
#2825=DIRECTION ( 'NONE',  ( 0.000000000000000000, 0.000000000000000000, 1.000000000000000000 ) ) ;
#2826=CARTESIAN_POINT ( 'NONE',  ( 6.502944117165512239, 24.14103883855864652, 35.54306285688424794 ) ) ;
#2830=CARTESIAN_POINT ( 'NONE',  ( 2.655777422895189144, -24.85958502782042601, 24.75666344040547884 ) ) ;
#2834=AXIS2_PLACEMENT_3D ( 'NONE', #4189, #3721, #763 ) ;
#2848=EDGE_CURVE ( 'NONE', #861, #5038, #5033, .T. ) ;
#2851=CARTESIAN_POINT ( 'NONE',  ( -2.226229255992760780, -22.89589894665499870, 24.59902000234163211 ) ) ;
#2856=EDGE_CURVE ( 'NONE', #1773, #6074, #3786, .T. ) ;
#2858=CARTESIAN_POINT ( 'NONE',  ( 3.337067332043157197, 24.78046181229916911, 25.04046888573288498 ) ) ;
#2860=DIRECTION ( 'NONE',  ( 0.000000000000000000, -1.000000000000000000, 0.000000000000000000 ) ) ;
#2861=AXIS2_PLACEMENT_3D ( 'NONE', #859, #4813, #4849 ) ;
#2862=CARTESIAN_POINT ( 'NONE',  ( 4.600626795032661143, -22.53777557106161922, 25.83521031145350122 ) ) ;
#2864=PRODUCT_DEFINITION ( 'UNKNOWN', '', #3754, #1316 ) ;
#2866=DIRECTION ( 'NONE',  ( 0.000000000000000000, 0.000000000000000000, -1.000000000000000000 ) ) ;
#2868=ORIENTED_EDGE ( 'NONE', *, *, #3538, .F. ) ;
#2869=CARTESIAN_POINT ( 'NONE',  ( -4.050825139678606135, 22.64130375691644304, 38.09092692957536030 ) ) ;
#2870=EDGE_CURVE ( 'NONE', #554, #3333, #3900, .T. ) ;
#2885=CARTESIAN_POINT ( 'NONE',  ( -4.258741324358278568, -24.63828325354172222, 9.488137494773077663 ) ) ;
#2892=ORIENTED_EDGE ( 'NONE', *, *, #358, .F. ) ;
#2895=DIRECTION ( 'NONE',  ( -1.000000000000000000, 0.000000000000000000, 0.000000000000000000 ) ) ;
#2911=APPLICATION_CONTEXT ( 'automotive_design' ) ;
#2912=CARTESIAN_POINT ( 'NONE',  ( -25.00000000000000000, 0.000000000000000000, 44.00000000000000711 ) ) ;
#2913=CARTESIAN_POINT ( 'NONE',  ( 4.322439664174057228, -24.63752030717468600, 9.487820034421874382 ) ) ;
#2925=CARTESIAN_POINT ( 'NONE',  ( 0.000000000000000000, 0.000000000000000000, 23.77500997278103512 ) ) ;
#2926=VERTEX_POINT ( 'NONE', #5853 ) ;
#2927=CARTESIAN_POINT ( 'NONE',  ( 6.810998761473115337, 21.97232263399875762, 8.650160397932937784 ) ) ;
#2940=VERTEX_POINT ( 'NONE', #2813 ) ;
#2949=CARTESIAN_POINT ( 'NONE',  ( 15.63375151319037037, -19.51424150167564875, 0.7397720130343804490 ) ) ;
#2957=DIRECTION ( 'NONE',  ( 0.000000000000000000, 0.000000000000000000, 1.000000000000000000 ) ) ;
#2962=CYLINDRICAL_SURFACE ( 'NONE', #4371, 22.00000000000000000 ) ;
#2963=DIRECTION ( 'NONE',  ( 0.000000000000000000, 0.000000000000000000, 1.000000000000000000 ) ) ;
#2966=DIRECTION ( 'NONE',  ( 0.000000000000000000, -1.000000000000000000, 0.000000000000000000 ) ) ;
#2970=ORIENTED_EDGE ( 'NONE', *, *, #3936, .T. ) ;
#2978=ORIENTED_EDGE ( 'NONE', *, *, #4013, .F. ) ;
#2984=DIRECTION ( 'NONE',  ( 0.000000000000000000, 0.000000000000000000, -1.000000000000000000 ) ) ;
#2986=CARTESIAN_POINT ( 'NONE',  ( 0.8953912278517150991, -24.98774879684975403, 9.982794782258027411 ) ) ;
#2998=EDGE_CURVE ( 'NONE', #4881, #1386, #5400, .T. ) ;
#3004=CARTESIAN_POINT ( 'NONE',  ( 13.87989846901268187, 18.35105360579683165, 3.366461006762181185 ) ) ;
#3020=DIRECTION ( 'NONE',  ( 0.000000000000000000, 0.000000000000000000, -1.000000000000000000 ) ) ;
#3023=ADVANCED_FACE ( 'NONE', ( #5432 ), #1527, .T. ) ;
#3024=EDGE_CURVE ( 'NONE', #2926, #5632, #5966, .T. ) ;
#3027=CARTESIAN_POINT ( 'NONE',  ( 0.000000000000000000, 0.000000000000000000, 50.00000000000000711 ) ) ;
#3033=CARTESIAN_POINT ( 'NONE',  ( 6.802364521716127044, 21.97126452515143313, 28.60827024242000149 ) ) ;
#3037=ORIENTED_EDGE ( 'NONE', *, *, #3331, .F. ) ;
#3056=EDGE_CURVE ( 'NONE', #4602, #1294, #2356, .T. ) ;
#3059=AXIS2_PLACEMENT_3D ( 'NONE', #430, #3713, #1846 ) ;
#3064=CARTESIAN_POINT ( 'NONE',  ( 7.472848606399997706, 21.75217170649850118, 32.55500807037982725 ) ) ;
#3067=CARTESIAN_POINT ( 'NONE',  ( 8.933863590510663144, 23.35242969744759733, 7.599770008932984489 ) ) ;
#3070=ORIENTED_EDGE ( 'NONE', *, *, #3608, .T. ) ;
#3072=EDGE_LOOP ( 'NONE', ( #4855, #4658, #1442, #5857 ) ) ;
#3079=CIRCLE ( 'NONE', #4303, 25.00000000000000000 ) ;
#3081=ORIENTED_EDGE ( 'NONE', *, *, #753, .F. ) ;
#3094=DIRECTION ( 'NONE',  ( -1.000000000000000000, 1.224646799147352961E-16, 0.000000000000000000 ) ) ;
#3096=CARTESIAN_POINT ( 'NONE',  ( 6.710385028064199453, 21.99961506306615178, 35.13225475196805547 ) ) ;
#3097=CARTESIAN_POINT ( 'NONE',  ( 5.896395598744648581, 24.30897383879703710, 9.016004279442030978 ) ) ;
#3112=ORIENTED_EDGE ( 'NONE', *, *, #2998, .T. ) ;
#3120=DIRECTION ( 'NONE',  ( -0.000000000000000000, -0.000000000000000000, -1.000000000000000000 ) ) ;
#3123=CARTESIAN_POINT ( 'NONE',  ( -1.568280873051609348, 22.94756140746006778, 24.43729500028611312 ) ) ;
#3124=CARTESIAN_POINT ( 'NONE',  ( -6.736323264042104242, 24.07882193050101449, 8.680799421305115615 ) ) ;
#3130=DIRECTION ( 'NONE',  ( -1.000000000000000000, 0.000000000000000000, 0.000000000000000000 ) ) ;
#3136=ORIENTED_EDGE ( 'NONE', *, *, #4360, .F. ) ;
#3138=CIRCLE ( 'NONE', #377, 20.00000000000000000 ) ;
#3139=DIRECTION ( 'NONE',  ( 0.000000000000000000, 0.000000000000000000, 1.000000000000000000 ) ) ;
#3142=FACE_OUTER_BOUND ( 'NONE', #3835, .T. ) ;
#3151=CARTESIAN_POINT ( 'NONE',  ( 1.353091841878393042, -19.95700839110197933, 39.15972426387312311 ) ) ;
#3155=CARTESIAN_POINT ( 'NONE',  ( 6.979603745006294879, 21.91560538710199779, 29.02082494059217765 ) ) ;
#3158=CARTESIAN_POINT ( 'NONE',  ( 11.89524262375574892, 21.99145298458226705, 5.444687415670879993 ) ) ;
#3164=DIRECTION ( 'NONE',  ( -0.000000000000000000, -0.000000000000000000, -1.000000000000000000 ) ) ;
#3169=ORIENTED_EDGE ( 'NONE', *, *, #5355, .F. ) ;
#3172=CARTESIAN_POINT ( 'NONE',  ( -12.25547752887834818, -19.46581264560981239, 5.111654144181065895 ) ) ;
#3183=CIRCLE ( 'NONE', #1752, 25.00000000000000000 ) ;
#3188=CARTESIAN_POINT ( 'NONE',  ( 5.121424986093042087, 22.42477833501277829, 37.27216187635247024 ) ) ;
#3192=CARTESIAN_POINT ( 'NONE',  ( 7.199721615955812837, -21.84420850452976026, 33.88807004839755166 ) ) ;
#3193=ORIENTED_EDGE ( 'NONE', *, *, #2303, .F. ) ;
#3205=CARTESIAN_POINT ( 'NONE',  ( -12.82303992477784860, -19.09670753041942959, 4.547733370409773990 ) ) ;
#3209=EDGE_CURVE ( 'NONE', #1679, #394, #3592, .T. ) ;
#3215=FACE_OUTER_BOUND ( 'NONE', #3072, .T. ) ;
#3216=CARTESIAN_POINT ( 'NONE',  ( -4.580917930799676796, -24.58016474715296340, 37.73350732204198721 ) ) ;
#3219=CARTESIAN_POINT ( 'NONE',  ( -12.24406280880444164, 19.48300239097275721, 5.141666792244760309 ) ) ;
#3221=CARTESIAN_POINT ( 'NONE',  ( 7.438449848406675002, 23.86776331625856784, 32.76532521224501693 ) ) ;
#3228=CARTESIAN_POINT ( 'NONE',  ( 13.85467998626346997, -20.81921389911401832, 3.398299129130501139 ) ) ;
#3236=CARTESIAN_POINT ( 'NONE',  ( 3.443445423526525051, -22.74486015987870147, 9.669004251864722121 ) ) ;
#3248=CARTESIAN_POINT ( 'NONE',  ( -1.953660101606557564, -24.92823101129173580, 24.51724137628377420 ) ) ;
#3253=CARTESIAN_POINT ( 'NONE',  ( 7.401918722292613495, 23.87915698552384924, 33.00856600121883133 ) ) ;
#3257=EDGE_CURVE ( 'NONE', #3828, #1896, #1111, .T. ) ;
#3259=CARTESIAN_POINT ( 'NONE',  ( 4.579678590235491065, -24.58038806634821682, 37.73441246790280701 ) ) ;
#3262=EDGE_CURVE ( 'NONE', #1020, #4754, #6355, .T. ) ;
#3263=CARTESIAN_POINT ( 'NONE',  ( -7.306265819825862096, 23.90859775135293219, 30.06340984243353276 ) ) ;
#3271=EDGE_CURVE ( 'NONE', #3765, #5357, #4419, .T. ) ;
#3273=CARTESIAN_POINT ( 'NONE',  ( -0.4786673552078670735, -22.99919074915722916, 9.998953803578743305 ) ) ;
#3274=CARTESIAN_POINT ( 'NONE',  ( 25.00000000000000000, 3.061616997868383043E-15, 55.00000000000000711 ) ) ;
#3286=EDGE_LOOP ( 'NONE', ( #4443, #4903, #5433, #593, #1943, #2317 ) ) ;
#3287=FACE_OUTER_BOUND ( 'NONE', #1505, .T. ) ;
#3288=CARTESIAN_POINT ( 'NONE',  ( 0.000000000000000000, 0.000000000000000000, 55.00000000000000711 ) ) ;
#3290=CARTESIAN_POINT ( 'NONE',  ( 0.000000000000000000, 0.000000000000000000, 47.00000000000000711 ) ) ;
#3291=CARTESIAN_POINT ( 'NONE',  ( 3.329879077396678877, -24.78142485916624693, 38.51307783140496355 ) ) ;
#3295=CARTESIAN_POINT ( 'NONE',  ( -4.574218739510392595, 24.57872545437487233, 25.82634213602822726 ) ) ;
#3296=CARTESIAN_POINT ( 'NONE',  ( 0.000000000000000000, 0.000000000000000000, 39.00000000000001421 ) ) ;
#3300=ORIENTED_EDGE ( 'NONE', *, *, #482, .F. ) ;
#3302=ORIENTED_EDGE ( 'NONE', *, *, #4879, .F. ) ;
#3306=DIRECTION ( 'NONE',  ( 0.000000000000000000, -1.000000000000000000, 0.000000000000000000 ) ) ;
#3310=CYLINDRICAL_SURFACE ( 'NONE', #294, 25.00000000000000000 ) ;
#3311=CARTESIAN_POINT ( 'NONE',  ( -7.246617758453442804, -23.92680898849839721, 29.82624669321133482 ) ) ;
#3314=CARTESIAN_POINT ( 'NONE',  ( 6.097143767825691008, 24.24550159253068671, 36.14924867743860659 ) ) ;
#3317=CARTESIAN_POINT ( 'NONE',  ( 4.375754180095211332, -24.61494036324241108, 25.67889403490024236 ) ) ;
#3320=CARTESIAN_POINT ( 'NONE',  ( -4.579678590235483959, 24.58038806634820972, 37.73441246790279990 ) ) ;
#3321=DIRECTION ( 'NONE',  ( -1.000000000000000000, 0.000000000000000000, 0.000000000000000000 ) ) ;
#3331=EDGE_CURVE ( 'NONE', #6017, #1209, #284, .T. ) ;
#3333=VERTEX_POINT ( 'NONE', #2063 ) ;
#3342=ADVANCED_FACE ( 'NONE', ( #5421 ), #5508, .T. ) ;
#3347=CARTESIAN_POINT ( 'NONE',  ( 2.425736827820245356, -24.88619925908220409, 38.88876102270705104 ) ) ;
#3365=B_SPLINE_CURVE_WITH_KNOTS ( 'NONE', 3,
 ( #491, #1453, #4412, #1511 ),
 .UNSPECIFIED., .F., .F.,
 ( 4, 4 ),
 ( 0.000000000000000000, 0.002032958594636732723 ),
 .UNSPECIFIED. ) ;
#3371=CARTESIAN_POINT ( 'NONE',  ( 0.000000000000000000, 0.000000000000000000, 39.00000000000001421 ) ) ;
#3373=CARTESIAN_POINT ( 'NONE',  ( -7.502604696612909407, -21.74191879359210944, 31.88172732429694989 ) ) ;
#3381=DIRECTION ( 'NONE',  ( 0.000000000000000000, 0.000000000000000000, 1.000000000000000000 ) ) ;
#3388=CARTESIAN_POINT ( 'NONE',  ( 7.443729366988918004E-21, -23.00000000000000000, 24.27501000028010125 ) ) ;
#3394=EDGE_LOOP ( 'NONE', ( #4764, #379, #6206, #348 ) ) ;
#3396=VERTEX_POINT ( 'NONE', #3417 ) ;
#3401=CARTESIAN_POINT ( 'NONE',  ( -3.415902643629519009, -24.76920443774479352, 9.674315651764088031 ) ) ;
#3405=CARTESIAN_POINT ( 'NONE',  ( -7.368286983821151992, -21.78790057683621129, 30.30389194166913569 ) ) ;
#3417=CARTESIAN_POINT ( 'NONE',  ( -25.00000000000000000, 0.000000000000000000, 47.00000000000000711 ) ) ;
#3420=CARTESIAN_POINT ( 'NONE',  ( -3.667391228670915382, 22.70656428659075843, 38.32101890234235242 ) ) ;
#3427=ORIENTED_EDGE ( 'NONE', *, *, #2795, .T. ) ;
#3429=CARTESIAN_POINT ( 'NONE',  ( 0.000000000000000000, 0.000000000000000000, 50.00000000000000711 ) ) ;
#3432=ORIENTED_EDGE ( 'NONE', *, *, #4883, .F. ) ;
#3440=VERTEX_POINT ( 'NONE', #5095 ) ;
#3453=EDGE_CURVE ( 'NONE', #116, #3948, #38, .T. ) ;
#3454=VECTOR ( 'NONE', #770, 1000.000000000000000 ) ;
#3455=DIRECTION ( 'NONE',  ( 0.000000000000000000, 0.000000000000000000, -1.000000000000000000 ) ) ;
#3480=CARTESIAN_POINT ( 'NONE',  ( 2.432532833620817403, 24.88553977760507152, 24.66355118963700832 ) ) ;
#3485=CARTESIAN_POINT ( 'NONE',  ( 15.99408614349810698, 16.52843635781563592, 0.000000000000000000 ) ) ;
#3494=ORIENTED_EDGE ( 'NONE', *, *, #753, .T. ) ;
#3497=ADVANCED_FACE ( 'NONE', ( #170 ), #3666, .F. ) ;
#3500=AXIS2_PLACEMENT_3D ( 'NONE', #2121, #4078, #4601 ) ;
#3507=CARTESIAN_POINT ( 'NONE',  ( -6.381573266039188397, -22.09732860014628031, 35.72159715675526570 ) ) ;
#3508=DIRECTION ( 'NONE',  ( 1.000000000000000000, 0.000000000000000000, 0.000000000000000000 ) ) ;
#3511=CARTESIAN_POINT ( 'NONE',  ( -25.00000000000000000, 0.000000000000000000, 55.00000000000000711 ) ) ;
#3518=CARTESIAN_POINT ( 'NONE',  ( 4.240673024049072204, 22.60901396202200075, 25.57291330172528987 ) ) ;
#3520=ADVANCED_FACE ( 'NONE', ( #2695 ), #138, .F. ) ;
#3525=ADVANCED_FACE ( 'NONE', ( #2634 ), #3571, .F. ) ;
#3526=CARTESIAN_POINT ( 'NONE',  ( 15.99408614349810698, -16.52843635781563592, 0.000000000000000000 ) ) ;
#3529=PLANE ( 'NONE',  #1221 ) ;
#3530=CARTESIAN_POINT ( 'NONE',  ( -13.84152781008413946, -20.82799749684992108, 3.414623522204553563 ) ) ;
#3536=CYLINDRICAL_SURFACE ( 'NONE', #834, 20.00000000000000000 ) ;
#3538=EDGE_CURVE ( 'NONE', #4754, #1020, #575, .T. ) ;
#3548=CARTESIAN_POINT ( 'NONE',  ( 7.502466904913718260, 21.74196656924153714, 31.65671859158186763 ) ) ;
#3550=DIRECTION ( 'NONE',  ( -0.000000000000000000, -0.000000000000000000, -1.000000000000000000 ) ) ;
#3555=DIRECTION ( 'NONE',  ( -0.000000000000000000, -0.000000000000000000, -1.000000000000000000 ) ) ;
#3557=DIRECTION ( 'NONE',  ( 0.000000000000000000, 0.000000000000000000, -1.000000000000000000 ) ) ;
#3571=PLANE ( 'NONE',  #1225 ) ;
#3573=CARTESIAN_POINT ( 'NONE',  ( -11.01859089670589675, 20.20136408472527023, 6.200517937480644726 ) ) ;
#3575=CARTESIAN_POINT ( 'NONE',  ( -5.578949544899560742, 22.31500106593816213, 26.74243945601464745 ) ) ;
#3576=VECTOR ( 'NONE', #6325, 1000.000000000000000 ) ;
#3577=CARTESIAN_POINT ( 'NONE',  ( 3.415902643629519009, 24.76920443774479352, 9.674315651764088031 ) ) ;
#3580=AXIS2_PLACEMENT_3D ( 'NONE', #5744, #2825, #6192 ) ;
#3581=ORIENTED_EDGE ( 'NONE', *, *, #5830, .F. ) ;
#3582=ORIENTED_EDGE ( 'NONE', *, *, #482, .T. ) ;
#3583=ORIENTED_EDGE ( 'NONE', *, *, #3271, .T. ) ;
#3588=CARTESIAN_POINT ( 'NONE',  ( 0.000000000000000000, 0.000000000000000000, 50.00000000000000711 ) ) ;
#3592=CIRCLE ( 'NONE', #4425, 23.00000000000000000 ) ;
#3595=ORIENTED_EDGE ( 'NONE', *, *, #2294, .T. ) ;
#3597=ORIENTED_EDGE ( 'NONE', *, *, #5263, .T. ) ;
#3603=ADVANCED_FACE ( 'NONE', ( #4216 ), #1994, .T. ) ;
#3608=EDGE_CURVE ( 'NONE', #1146, #4872, #3183, .T. ) ;
#3609=CARTESIAN_POINT ( 'NONE',  ( -7.512701611559312376, 21.73844013154226218, 31.66439142681324981 ) ) ;
#3616=EDGE_LOOP ( 'NONE', ( #3432, #4028, #5280, #766, #1606, #1072, #3081 ) ) ;
#3618=DIRECTION ( 'NONE',  ( 0.000000000000000000, 1.000000000000000000, 0.000000000000000000 ) ) ;
#3622=CARTESIAN_POINT ( 'NONE',  ( -12.76907600075766247, -21.49559483975649599, 4.603672158788645774 ) ) ;
#3625=CARTESIAN_POINT ( 'NONE',  ( -2.876010458515648960, -22.82309565144259267, 38.71608687161452877 ) ) ;
#3626=VERTEX_POINT ( 'NONE', #33 ) ;
#3636=PRODUCT_DEFINITION_SHAPE ( 'NONE', 'NONE',  #2864 ) ;
#3638=CARTESIAN_POINT ( 'NONE',  ( 5.575863217335945698, 22.31445838370337853, 26.75407420319146823 ) ) ;
#3640=CARTESIAN_POINT ( 'NONE',  ( -10.34785354329971341, 22.76990768458740177, 6.703770685560594522 ) ) ;
#3641=CARTESIAN_POINT ( 'NONE',  ( 6.716176415091607232, -21.99834172012562661, 35.14285310556104491 ) ) ;
#3642=ORIENTED_EDGE ( 'NONE', *, *, #4275, .T. ) ;
#3644=ORIENTED_EDGE ( 'NONE', *, *, #196, .F. ) ;
#3652=VECTOR ( 'NONE', #2118, 1000.000000000000000 ) ;
#3654=CARTESIAN_POINT ( 'NONE',  ( 4.711348314259845793, -22.51623045471248119, 9.370182291681606657 ) ) ;
#3658=CIRCLE ( 'NONE', #1400, 25.00000000000000000 ) ;
#3662=UNCERTAINTY_MEASURE_WITH_UNIT (LENGTH_MEASURE( 1.000000000000000082E-05 ), #2204, 'distance_accuracy_value', 'NONE');
#3665=CARTESIAN_POINT ( 'NONE',  ( 22.00000000000000000, 2.694222958124176809E-15, 44.00000000000000711 ) ) ;
#3666=CYLINDRICAL_SURFACE ( 'NONE', #3500, 23.00000000000000000 ) ;
#3669=CARTESIAN_POINT ( 'NONE',  ( 0.000000000000000000, 0.000000000000000000, 55.00000000000000711 ) ) ;
#3671=CARTESIAN_POINT ( 'NONE',  ( 2.012341796004660122, 22.91179784512888773, 39.00000000000001421 ) ) ;
#3673=CARTESIAN_POINT ( 'NONE',  ( 4.673148220383224860, 24.56288069930688067, 9.380541037249376046 ) ) ;
#3674=CARTESIAN_POINT ( 'NONE',  ( 4.050825139678606135, -22.64130375691644304, 38.09092692957536030 ) ) ;
#3679=CARTESIAN_POINT ( 'NONE',  ( -1.948881123199609711, 24.92505092879368078, 24.52843033598424327 ) ) ;
#3680=LINE ( 'NONE', #1297, #4693 ) ;
#3681=DIRECTION ( 'NONE',  ( 1.000000000000000000, 0.000000000000000000, 0.000000000000000000 ) ) ;
#3686=LINE ( 'NONE', #3904, #4710 ) ;
#3687=ORIENTED_EDGE ( 'NONE', *, *, #1911, .F. ) ;
#3705=CARTESIAN_POINT ( 'NONE',  ( 1.684770966858813335, -19.93163181623162572, 39.09123673121591480 ) ) ;
#3708=VERTEX_POINT ( 'NONE', #4372 ) ;
#3709=CARTESIAN_POINT ( 'NONE',  ( 7.500037790182079611, 23.84846815096122796, 31.28125562555190342 ) ) ;
#3710=DIRECTION ( 'NONE',  ( 0.000000000000000000, 0.000000000000000000, 1.000000000000000000 ) ) ;
#3713=DIRECTION ( 'NONE',  ( 0.000000000000000000, 0.000000000000000000, 1.000000000000000000 ) ) ;
#3716=CARTESIAN_POINT ( 'NONE',  ( 2.012341796004660122, -22.91179784512888773, 39.00000000000001421 ) ) ;
#3720=ADVANCED_FACE ( 'NONE', ( #3 ), #1450, .F. ) ;
#3721=DIRECTION ( 'NONE',  ( 0.000000000000000000, 0.000000000000000000, -1.000000000000000000 ) ) ;
#3723=LINE ( 'NONE', #703, #4510 ) ;
#3726=DIRECTION ( 'NONE',  ( 0.000000000000000000, -1.000000000000000000, 0.000000000000000000 ) ) ;
#3731=CARTESIAN_POINT ( 'NONE',  ( -6.012884121744077603, -22.20400618356517697, 8.958536348443306707 ) ) ;
#3738=VECTOR ( 'NONE', #5645, 1000.000000000000000 ) ;
#3739=DIRECTION ( 'NONE',  ( 1.000000000000000000, 0.000000000000000000, 0.000000000000000000 ) ) ;
#3743=CARTESIAN_POINT ( 'NONE',  ( -5.475713916123538638, -24.39360375241166778, 36.90593746307732204 ) ) ;
#3746=CARTESIAN_POINT ( 'NONE',  ( 9.185524248261779151E-16, 25.00000000000000000, 39.27501000028010480 ) ) ;
#3750=CARTESIAN_POINT ( 'NONE',  ( 5.648970382492173314, -24.35596037157666771, 26.81763994746972912 ) ) ;
#3753=CARTESIAN_POINT ( 'NONE',  ( -2.425736827820241803, 24.88619925908220054, 38.88876102270705815 ) ) ;
#3754=PRODUCT_DEFINITION_FORMATION_WITH_SPECIFIED_SOURCE ( 'ANY', '', #4667, .NOT_KNOWN. ) ;
#3761=CARTESIAN_POINT ( 'NONE',  ( -10.40746208496127245, -20.52425257667962555, 6.660905398399123101 ) ) ;
#3764=CARTESIAN_POINT ( 'NONE',  ( 2.012341796004660122, -19.89850447888114005, 39.00000000000001421 ) ) ;
#3765=VERTEX_POINT ( 'NONE', #5995 ) ;
#3767=B_SPLINE_CURVE_WITH_KNOTS ( 'NONE', 3,
 ( #4188, #270, #824, #3783, #3679, #5201, #1295, #307, #4228, #792, #3295, #5235, #1782, #4677, #2705, #5757, #1329, #2809, #5274, #4778, #3263, #5174, #372, #2737, #762, #2293, #2327, #4288, #2225, #6265, #1853, #408, #2773, #4747, #5788, #1364, #3320, #2260, #5300, #3753, #886, #1709, #5652, #343, #5718, #1231 ),
 .UNSPECIFIED., .F., .F.,
 ( 4, 2, 2, 2, 2, 2, 2, 2, 2, 2, 2, 2, 2, 2, 2, 2, 2, 2, 2, 2, 2, 2, 4 ),
 ( 2.472553540688041407E-19, 0.001474063385043944061, 0.002211095077565916091, 0.002948126770087888121, 0.004422190155131833049, 0.005159221847653804212, 0.005896253540175776242, 0.007370316925219718568, 0.008844380310263660894, 0.009581412002785630322, 0.01031844369530760148, 0.01179250708035154208, 0.01326657046539548267, 0.01474063385043942499, 0.01547766554296140483, 0.01621469723548338293, 0.01695172892800536277, 0.01768876062052734260, 0.01916282400557132309, 0.02063688739061530358, 0.02211095077565928407, 0.02284798246818127432, 0.02358501416070326803 ),
 .UNSPECIFIED. ) ;
#3772=CARTESIAN_POINT ( 'NONE',  ( -3.330617891528921515, -24.78132568362454435, 38.51271458136145753 ) ) ;
#3773=ORIENTED_EDGE ( 'NONE', *, *, #5618, .T. ) ;
#3775=CARTESIAN_POINT ( 'NONE',  ( 25.00000000000000000, 3.061616997868383043E-15, 55.00000000000000711 ) ) ;
#3776=ORIENTED_EDGE ( 'NONE', *, *, #2848, .F. ) ;
#3777=CARTESIAN_POINT ( 'NONE',  ( -1.684770966858812891, 19.93163181623162572, 39.09123673121591480 ) ) ;
#3778=CARTESIAN_POINT ( 'NONE',  ( 2.450084894395748503, 22.87335089571185875, 38.87807751528530531 ) ) ;
#3780=CARTESIAN_POINT ( 'NONE',  ( 3.769188925537579671, -24.71764851934220175, 38.27740560533010949 ) ) ;
#3783=CARTESIAN_POINT ( 'NONE',  ( -1.710351842506663500, 24.94259032362968398, 24.46851125284992179 ) ) ;
#3786=LINE ( 'NONE', #1432, #308 ) ;
#3796=CIRCLE ( 'NONE', #1105, 25.00000000000000000 ) ;
#3798=DIRECTION ( 'NONE',  ( -1.000000000000000000, 0.000000000000000000, 0.000000000000000000 ) ) ;
#3800=CARTESIAN_POINT ( 'NONE',  ( -4.376116820636601012, -24.61487579939255710, 25.67915452354946737 ) ) ;
#3804=CARTESIAN_POINT ( 'NONE',  ( 5.641746473127992267, 24.35561814371764910, 36.72278580929200587 ) ) ;
#3808=DIRECTION ( 'NONE',  ( 0.000000000000000000, 0.000000000000000000, 1.000000000000000000 ) ) ;
#3809=CARTESIAN_POINT ( 'NONE',  ( 1.957817464472357827, -24.92794428843966514, 39.03180047523677842 ) ) ;
#3820=ORIENTED_EDGE ( 'NONE', *, *, #3056, .F. ) ;
#3823=ADVANCED_FACE ( 'NONE', ( #3142 ), #1633, .F. ) ;
#3827=DIRECTION ( 'NONE',  ( 1.000000000000000000, 0.000000000000000000, 0.000000000000000000 ) ) ;
#3828=VERTEX_POINT ( 'NONE', #1109 ) ;
#3830=DIRECTION ( 'NONE',  ( 0.000000000000000000, -1.000000000000000000, 0.000000000000000000 ) ) ;
#3833=CARTESIAN_POINT ( 'NONE',  ( -23.00000000000000000, 0.000000000000000000, 0.000000000000000000 ) ) ;
#3834=CARTESIAN_POINT ( 'NONE',  ( -2.546401178541497462E-16, -25.00000000000000000, 24.27501000028010125 ) ) ;
#3835=EDGE_LOOP ( 'NONE', ( #279, #4252, #5172, #3193, #2602, #5401 ) ) ;
#3838=CARTESIAN_POINT ( 'NONE',  ( 3.766262172602996561, 24.71811694763050937, 25.27080528860306430 ) ) ;
#3839=FACE_OUTER_BOUND ( 'NONE', #3973, .T. ) ;
#3840=CARTESIAN_POINT ( 'NONE',  ( 5.269070065585171214, -22.39093555978999817, 26.41927588677976502 ) ) ;
#3842=CARTESIAN_POINT ( 'NONE',  ( 0.000000000000000000, 0.000000000000000000, 39.00000000000001421 ) ) ;
#3844=DIRECTION ( 'NONE',  ( -1.000000000000000000, 0.000000000000000000, 0.000000000000000000 ) ) ;
#3856=SHAPE_REPRESENTATION_RELATIONSHIP ( 'NONE' , 'NONE' ,  #1490, #4941 ) ;
#3857=CARTESIAN_POINT ( 'NONE',  ( -7.502466904913718260, -21.74196656924153714, 31.65671859158186763 ) ) ;
#3864=CARTESIAN_POINT ( 'NONE',  ( 5.133588784792091353, 24.46788053448572242, 26.30186172257456789 ) ) ;
#3866=CARTESIAN_POINT ( 'NONE',  ( 7.257770128441434210, -23.92352318576051928, 33.72861583961353205 ) ) ;
#3868=DIRECTION ( 'NONE',  ( -0.000000000000000000, -0.000000000000000000, -1.000000000000000000 ) ) ;
#3869=VERTEX_POINT ( 'NONE', #6085 ) ;
#3870=CARTESIAN_POINT ( 'NONE',  ( -6.505027467542590536, 22.06241888168487009, 35.53465933272089927 ) ) ;
#3883=CARTESIAN_POINT ( 'NONE',  ( 15.23040061807463630, -19.83277885499231630, 1.438641001509332051 ) ) ;
#3890=ADVANCED_FACE ( 'NONE', ( #6054 ), #3536, .F. ) ;
#3895=FACE_OUTER_BOUND ( 'NONE', #2274, .T. ) ;
#3897=FACE_BOUND ( 'NONE', #989, .T. ) ;
#3900=CIRCLE ( 'NONE', #4724, 25.00000000000000000 ) ;
#3903=CIRCLE ( 'NONE', #2250, 25.00000000000000000 ) ;
#3904=CARTESIAN_POINT ( 'NONE',  ( 9.184850993605147944E-16, 25.00000000000000000, 39.27501000028010480 ) ) ;
#3907=CYLINDRICAL_SURFACE ( 'NONE', #445, 25.00000000000000000 ) ;
#3911=ORIENTED_EDGE ( 'NONE', *, *, #1205, .F. ) ;
#3918=DIRECTION ( 'NONE',  ( -0.000000000000000000, -0.000000000000000000, -1.000000000000000000 ) ) ;
#3921=CIRCLE ( 'NONE', #538, 22.00000000000000000 ) ;
#3922=VECTOR ( 'NONE', #4916, 1000.000000000000000 ) ;
#3936=EDGE_CURVE ( 'NONE', #1346, #554, #5154, .T. ) ;
#3948=VERTEX_POINT ( 'NONE', #3764 ) ;
#3954=CARTESIAN_POINT ( 'NONE',  ( 8.983986218495337184, -23.34169575125378771, 7.586426789398496240 ) ) ;
#3957=CARTESIAN_POINT ( 'NONE',  ( -7.058581574212176690, -21.89022081680645826, 29.23014371996821481 ) ) ;
#3966=CARTESIAN_POINT ( 'NONE',  ( -25.00000000000000000, 0.000000000000000000, 50.00000000000000711 ) ) ;
#3967=CIRCLE ( 'NONE', #4265, 23.00000000000000000 ) ;
#3968=CARTESIAN_POINT ( 'NONE',  ( -5.116921499885075164, 22.42580359959007552, 37.27629952662707069 ) ) ;
#3973=EDGE_LOOP ( 'NONE', ( #5553, #4330, #519, #807, #5087, #5901 ) ) ;
#3979=CARTESIAN_POINT ( 'NONE',  ( -2.985931097914281462, -24.82479382442820537, 9.752995572818681680 ) ) ;
#3982=CARTESIAN_POINT ( 'NONE',  ( -4.781067518356564072, -22.50057576469317411, 37.57069195157705366 ) ) ;
#3986=VECTOR ( 'NONE', #2151, 1000.000000000000000 ) ;
#3988=DIRECTION ( 'NONE',  ( 0.000000000000000000, 0.000000000000000000, 1.000000000000000000 ) ) ;
#3991=EDGE_CURVE ( 'NONE', #414, #4976, #532, .T. ) ;
#3993=CARTESIAN_POINT ( 'NONE',  ( -0.8980764441730644254, 22.98681745009828248, 24.31513574047610504 ) ) ;
#4005=ADVANCED_FACE ( 'NONE', ( #5799 ), #897, .T. ) ;
#4010=AXIS2_PLACEMENT_3D ( 'NONE', #1307, #2716, #3827 ) ;
#4013=EDGE_CURVE ( 'NONE', #2940, #1460, #1830, .T. ) ;
#4019=B_SPLINE_CURVE_WITH_KNOTS ( 'NONE', 3,
 ( #850, #2802, #4312, #1810, #3777, #4772 ),
 .UNSPECIFIED., .F., .F.,
 ( 4, 2, 4 ),
 ( 0.002032958594636732723, 0.003043324567219493192, 0.004053690539802253662 ),
 .UNSPECIFIED. ) ;
#4025=CARTESIAN_POINT ( 'NONE',  ( 0.9006954679665252206, 22.98346407483541753, 24.32584948309267148 ) ) ;
#4028=ORIENTED_EDGE ( 'NONE', *, *, #2769, .T. ) ;
#4038=CARTESIAN_POINT ( 'NONE',  ( -5.121424986093042087, -22.42477833501277829, 37.27216187635247024 ) ) ;
#4042=CARTESIAN_POINT ( 'NONE',  ( 0.000000000000000000, 0.000000000000000000, 39.00000000000001421 ) ) ;
#4046=CARTESIAN_POINT ( 'NONE',  ( 0.4786673552078670735, 22.99919074915722916, 9.998953803578743305 ) ) ;
#4048=CARTESIAN_POINT ( 'NONE',  ( -2.223777455422794702, 22.89327810718596368, 24.60873847605252251 ) ) ;
#4049=CARTESIAN_POINT ( 'NONE',  ( 6.685354258535094907, 24.10283321907682108, 8.717551967824453740 ) ) ;
#4055=EDGE_LOOP ( 'NONE', ( #1840, #3597, #1132, #761 ) ) ;
#4059=CARTESIAN_POINT ( 'NONE',  ( 23.00000000000000000, 2.816687638038912352E-15, 39.00000000000001421 ) ) ;
#4066=CARTESIAN_POINT ( 'NONE',  ( 1.908796811648538206E-15, -20.00000000000000711, 39.27501000028011902 ) ) ;
#4068=ADVANCED_FACE ( 'NONE', ( #2434, #6312 ), #1050, .T. ) ;
#4075=DIRECTION ( 'NONE',  ( 0.000000000000000000, 0.000000000000000000, -1.000000000000000000 ) ) ;
#4078=DIRECTION ( 'NONE',  ( -0.000000000000000000, -0.000000000000000000, -1.000000000000000000 ) ) ;
#4082=CARTESIAN_POINT ( 'NONE',  ( 6.703552034654557623, 22.00169986843530268, 28.40415011795442979 ) ) ;
#4084=CARTESIAN_POINT ( 'NONE',  ( -15.63375151319036682, 19.51424150167564520, 0.7397720130343804490 ) ) ;
#4088=EDGE_LOOP ( 'NONE', ( #2100, #3642, #5515, #4686, #5096, #1094 ) ) ;
#4096=CARTESIAN_POINT ( 'NONE',  ( -15.99408614349810698, -19.21429697996681440, -4.336808689942017736E-15 ) ) ;
#4103=EDGE_CURVE ( 'NONE', #1346, #5357, #64, .T. ) ;
#4112=CARTESIAN_POINT ( 'NONE',  ( 2.012341796004660122, -19.89850447888114005, 39.00000000000001421 ) ) ;
#4116=CARTESIAN_POINT ( 'NONE',  ( 7.071085268539269109, 21.88683845148715079, 34.31457501568616664 ) ) ;
#4118=CARTESIAN_POINT ( 'NONE',  ( -5.542644329336979148, 24.38138258431391847, 9.119897054702294170 ) ) ;
#4119=CARTESIAN_POINT ( 'NONE',  ( 6.135028333862784677, -22.16704433745741554, 36.09490741883096376 ) ) ;
#4126=LINE ( 'NONE', #6133, #309 ) ;
#4130=CARTESIAN_POINT ( 'NONE',  ( 0.8355139846970627282, -23.00151096327411793, 10.00195343045036189 ) ) ;
#4134=ORIENTED_EDGE ( 'NONE', *, *, #1593, .F. ) ;
#4161=CARTESIAN_POINT ( 'NONE',  ( 14.34541152806172626, -17.98734769216428830, 2.761683449857409656 ) ) ;
#4169=DIRECTION ( 'NONE',  ( 1.000000000000000000, 0.000000000000000000, 0.000000000000000000 ) ) ;
#4172=CARTESIAN_POINT ( 'NONE',  ( 0.000000000000000000, 0.000000000000000000, 39.00000000000001421 ) ) ;
#4174=( GEOMETRIC_REPRESENTATION_CONTEXT ( 3 ) GLOBAL_UNCERTAINTY_ASSIGNED_CONTEXT ( ( #136 ) ) GLOBAL_UNIT_ASSIGNED_CONTEXT ( ( #2437, #449, #6315 ) ) REPRESENTATION_CONTEXT ( 'NONE', 'WORKASPACE' ) );
#4175=CARTESIAN_POINT ( 'NONE',  ( -15.99408614349810698, 16.52843635781563592, 0.000000000000000000 ) ) ;
#4176=ORIENTED_EDGE ( 'NONE', *, *, #2870, .T. ) ;
#4178=CARTESIAN_POINT ( 'NONE',  ( 2.426466830553629439, 24.88612820222271438, 38.88851386838336310 ) ) ;
#4182=CARTESIAN_POINT ( 'NONE',  ( 14.33006727100665856, 20.49285708348135415, 2.782958588747960427 ) ) ;
#4183=CARTESIAN_POINT ( 'NONE',  ( 7.471932569767337995, -21.75248695045747382, 32.56440574765390039 ) ) ;
#4186=ORIENTED_EDGE ( 'NONE', *, *, #865, .T. ) ;
#4188=CARTESIAN_POINT ( 'NONE',  ( 2.546401178541497462E-16, 25.00000000000000000, 24.27501000028010125 ) ) ;
#4189=CARTESIAN_POINT ( 'NONE',  ( 0.000000000000000000, 0.000000000000000000, 0.000000000000000000 ) ) ;
#4205=ORIENTED_EDGE ( 'NONE', *, *, #4345, .T. ) ;
#4206=VECTOR ( 'NONE', #438, 1000.000000000000000 ) ;
#4207=CARTESIAN_POINT ( 'NONE',  ( 0.000000000000000000, 0.000000000000000000, 0.000000000000000000 ) ) ;
#4216=FACE_OUTER_BOUND ( 'NONE', #413, .T. ) ;
#4225=CARTESIAN_POINT ( 'NONE',  ( 4.955340051326921902, -24.50653216723388894, 37.42604413602553137 ) ) ;
#4228=CARTESIAN_POINT ( 'NONE',  ( -3.765864371162154889, 24.71817793568963495, 25.27057431607724780 ) ) ;
#4232=ORIENTED_EDGE ( 'NONE', *, *, #5705, .F. ) ;
#4243=CARTESIAN_POINT ( 'NONE',  ( -6.502944117165513127, -24.14103883855863941, 35.54306285688424794 ) ) ;
#4247=CARTESIAN_POINT ( 'NONE',  ( 7.019376005445150390, 23.99453911528665984, 29.12205218481382829 ) ) ;
#4248=CARTESIAN_POINT ( 'NONE',  ( 2.876010458515648960, 22.82309565144259267, 38.71608687161452877 ) ) ;
#4250=CARTESIAN_POINT ( 'NONE',  ( 5.958341177435918290, -24.28123298992124290, 27.19342269918141852 ) ) ;
#4252=ORIENTED_EDGE ( 'NONE', *, *, #4013, .T. ) ;
#4256=DIRECTION ( 'NONE',  ( 0.000000000000000000, 0.000000000000000000, 1.000000000000000000 ) ) ;
#4262=EDGE_LOOP ( 'NONE', ( #3581, #4232 ) ) ;
#4264=ORIENTED_EDGE ( 'NONE', *, *, #1611, .F. ) ;
#4265=AXIS2_PLACEMENT_3D ( 'NONE', #4042, #4075, #2090 ) ;
#4273=CARTESIAN_POINT ( 'NONE',  ( -3.766262172602994340, -24.71811694763051293, 25.27080528860306430 ) ) ;
#4275=EDGE_CURVE ( 'NONE', #116, #4754, #3686, .T. ) ;
#4279=CARTESIAN_POINT ( 'NONE',  ( 0.4912064067414986801, 25.00000000000000711, 39.27501000028010480 ) ) ;
#4281=CARTESIAN_POINT ( 'NONE',  ( 0.000000000000000000, 0.000000000000000000, 44.00000000000000711 ) ) ;
#4283=CARTESIAN_POINT ( 'NONE',  ( 5.640759563529097242, -24.35584729907773749, 36.72391480687588228 ) ) ;
#4288=CARTESIAN_POINT ( 'NONE',  ( -6.830924868230225044, 24.04887075291641452, 34.88135594814352913 ) ) ;
#4298=CARTESIAN_POINT ( 'NONE',  ( 25.00000000000000000, 3.061616997868383043E-15, 0.000000000000000000 ) ) ;
#4303=AXIS2_PLACEMENT_3D ( 'NONE', #2136, #6080, #5622 ) ;
#4308=CARTESIAN_POINT ( 'NONE',  ( -5.133588784792095794, -24.46788053448571176, 26.30186172257456079 ) ) ;
#4311=AXIS2_PLACEMENT_3D ( 'NONE', #2925, #4902, #559 ) ;
#4312=CARTESIAN_POINT ( 'NONE',  ( -0.6815295361380612205, 19.99121204295638776, 39.25166565497248428 ) ) ;
#4313=CARTESIAN_POINT ( 'NONE',  ( 2.012341796004660122, 19.89850447888114005, 39.00000000000001421 ) ) ;
#4317=CARTESIAN_POINT ( 'NONE',  ( 5.474672603935804460, -24.39383812260185636, 36.90705202433115772 ) ) ;
#4324=MECHANICAL_DESIGN_GEOMETRIC_PRESENTATION_REPRESENTATION('',(#4631),#739);
#4327=DIRECTION ( 'NONE',  ( 0.000000000000000000, 0.000000000000000000, 1.000000000000000000 ) ) ;
#4330=ORIENTED_EDGE ( 'NONE', *, *, #3453, .T. ) ;
#4332=FACE_OUTER_BOUND ( 'NONE', #4055, .T. ) ;
#4334=CARTESIAN_POINT ( 'NONE',  ( 10.99369682877389387, -22.46365890119677999, 6.219949983291193973 ) ) ;
#4343=FACE_OUTER_BOUND ( 'NONE', #459, .T. ) ;
#4344=CARTESIAN_POINT ( 'NONE',  ( 0.000000000000000000, 0.000000000000000000, 44.00000000000000711 ) ) ;
#4345=EDGE_CURVE ( 'NONE', #3440, #3708, #4921, .T. ) ;
#4347=CARTESIAN_POINT ( 'NONE',  ( 4.574218739510392595, -24.57872545437487588, 25.82634213602822726 ) ) ;
#4349=DIRECTION ( 'NONE',  ( -1.000000000000000000, 0.000000000000000000, 0.000000000000000000 ) ) ;
#4352=CARTESIAN_POINT ( 'NONE',  ( -6.002163747819661666, 22.20348677930560655, 36.27767814654681899 ) ) ;
#4360=EDGE_CURVE ( 'NONE', #5193, #1679, #5847, .T. ) ;
#4365=CARTESIAN_POINT ( 'NONE',  ( 5.944036167333010212, -24.28654258472968408, 8.982995935198122339 ) ) ;
#4366=ORIENTED_EDGE ( 'NONE', *, *, #1201, .T. ) ;
#4369=CARTESIAN_POINT ( 'NONE',  ( -4.599867106623924506, -22.53795783706889821, 25.83444357079220666 ) ) ;
#4370=DIRECTION ( 'NONE',  ( 1.000000000000000000, 0.000000000000000000, -0.000000000000000000 ) ) ;
#4371=AXIS2_PLACEMENT_3D ( 'NONE', #5295, #943, #2895 ) ;
#4372=CARTESIAN_POINT ( 'NONE',  ( -2.012341796004660122, 19.89850447888114005, 39.00000000000001421 ) ) ;
#4377=CARTESIAN_POINT ( 'NONE',  ( 1.953660101606555122, 24.92823101129173580, 24.51724137628377420 ) ) ;
#4381=EDGE_LOOP ( 'NONE', ( #1909, #3582, #3070, #4771 ) ) ;
#4383=CYLINDRICAL_SURFACE ( 'NONE', #1420, 25.00000000000000000 ) ;
#4387=CARTESIAN_POINT ( 'NONE',  ( -2.546401178541497462E-16, -25.00000000000000000, 24.27501000028010125 ) ) ;
#4389=ADVANCED_FACE ( 'NONE', ( #433, #4718 ), #4383, .T. ) ;
#4394=ORIENTED_EDGE ( 'NONE', *, *, #4883, .T. ) ;
#4395=AXIS2_PLACEMENT_3D ( 'NONE', #6046, #6317, #3739 ) ;
#4398=DIRECTION ( 'NONE',  ( -0.000000000000000000, -0.000000000000000000, -1.000000000000000000 ) ) ;
#4402=CARTESIAN_POINT ( 'NONE',  ( -11.89524262375575603, -21.99145298458226705, 5.444687415670875552 ) ) ;
#4407=CARTESIAN_POINT ( 'NONE',  ( -23.00000000000000000, 0.000000000000000000, 39.00000000000001421 ) ) ;
#4409=AXIS2_PLACEMENT_3D ( 'NONE', #3669, #3120, #5097 ) ;
#4410=CARTESIAN_POINT ( 'NONE',  ( 0.000000000000000000, 0.000000000000000000, 39.00000000000001421 ) ) ;
#4412=CARTESIAN_POINT ( 'NONE',  ( 0.6825543444542561122, 20.00000000000000000, 39.27501000028010480 ) ) ;
#4413=EDGE_LOOP ( 'NONE', ( #5306, #4394 ) ) ;
#4416=CIRCLE ( 'NONE', #1632, 20.00000000000000000 ) ;
#4419=LINE ( 'NONE', #5481, #829 ) ;
#4420=ORIENTED_EDGE ( 'NONE', *, *, #791, .T. ) ;
#4425=AXIS2_PLACEMENT_3D ( 'NONE', #2612, #5068, #1191 ) ;
#4429=ORIENTED_EDGE ( 'NONE', *, *, #944, .T. ) ;
#4433=CIRCLE ( 'NONE', #4842, 22.00000000000000000 ) ;
#4435=DIRECTION ( 'NONE',  ( -1.000000000000000000, 0.000000000000000000, -0.000000000000000000 ) ) ;
#4436=CARTESIAN_POINT ( 'NONE',  ( 13.06023069425439864, -21.31967003585101850, 4.296371343529789222 ) ) ;
#4440=CARTESIAN_POINT ( 'NONE',  ( -6.137861079775116302, -22.16774101882030124, 27.44213700196646144 ) ) ;
#4442=ORIENTED_EDGE ( 'NONE', *, *, #5347, .F. ) ;
#4443=ORIENTED_EDGE ( 'NONE', *, *, #5263, .F. ) ;
#4446=CARTESIAN_POINT ( 'NONE',  ( 4.376116820636602789, 24.61487579939255355, 25.67915452354946737 ) ) ;
#4450=CARTESIAN_POINT ( 'NONE',  ( 25.00000000000000000, 3.061616997868383043E-15, 50.00000000000000711 ) ) ;
#4455=CARTESIAN_POINT ( 'NONE',  ( 15.99408614349810698, 16.52843635781563592, 0.000000000000000000 ) ) ;
#4462=CARTESIAN_POINT ( 'NONE',  ( -8.933863590510668473, -23.35242969744760089, 7.599770008932984489 ) ) ;
#4463=EDGE_LOOP ( 'NONE', ( #5675, #4535, #3820 ) ) ;
#4466=CARTESIAN_POINT ( 'NONE',  ( -1.127325861074953917, -22.97343572093476638, 24.35677350376877470 ) ) ;
#4467=DIRECTION ( 'NONE',  ( 0.000000000000000000, -1.000000000000000000, 0.000000000000000000 ) ) ;
#4477=DIRECTION ( 'NONE',  ( 0.000000000000000000, 0.000000000000000000, 1.000000000000000000 ) ) ;
#4479=CARTESIAN_POINT ( 'NONE',  ( -4.240260142090316542, 22.60916465144881826, 25.57229111368760854 ) ) ;
#4493=ORIENTED_EDGE ( 'NONE', *, *, #5830, .T. ) ;
#4509=CARTESIAN_POINT ( 'NONE',  ( -6.703346455576358665, 22.00175929117281015, 28.40382332099657958 ) ) ;
#4510=VECTOR ( 'NONE', #5686, 1000.000000000000000 ) ;
#4513=DIRECTION ( 'NONE',  ( -1.000000000000000000, 0.000000000000000000, 0.000000000000000000 ) ) ;
#4516=ORIENTED_EDGE ( 'NONE', *, *, #5270, .T. ) ;
#4530=VERTEX_POINT ( 'NONE', #4450 ) ;
#4535=ORIENTED_EDGE ( 'NONE', *, *, #4546, .T. ) ;
#4536=CARTESIAN_POINT ( 'NONE',  ( 10.40746208496127245, 20.52425257667962555, 6.660905398399123101 ) ) ;
#4538=CARTESIAN_POINT ( 'NONE',  ( -6.139315947428367615, 22.16738032098082911, 27.44370026704754650 ) ) ;
#4539=CARTESIAN_POINT ( 'NONE',  ( -2.201053925086813301, 24.90665284231785392, 9.868642342566225523 ) ) ;
#4544=EDGE_CURVE ( 'NONE', #5570, #1386, #150, .T. ) ;
#4546=EDGE_CURVE ( 'NONE', #3869, #1294, #717, .T. ) ;
#4553=EDGE_CURVE ( 'NONE', #4872, #1146, #3796, .T. ) ;
#4555=CARTESIAN_POINT ( 'NONE',  ( -13.04517011400474580, -21.32889776003924709, 4.312637851115566967 ) ) ;
#4563=ADVANCED_FACE ( 'NONE', ( #2697 ), #2125, .T. ) ;
#4571=CARTESIAN_POINT ( 'NONE',  ( -7.369598735940123824, 21.78745483514939707, 30.31133554494096671 ) ) ;
#4572=CARTESIAN_POINT ( 'NONE',  ( -12.78450670028659530, 21.48642263404484964, 4.587769495204019776 ) ) ;
#4601=DIRECTION ( 'NONE',  ( -1.000000000000000000, 0.000000000000000000, 0.000000000000000000 ) ) ;
#4602=VERTEX_POINT ( 'NONE', #3775 ) ;
#4603=EDGE_CURVE ( 'NONE', #53, #5357, #1844, .T. ) ;
#4606=CARTESIAN_POINT ( 'NONE',  ( 5.735021534702854140, 22.27575375288411408, 36.62858606677772144 ) ) ;
#4608=CARTESIAN_POINT ( 'NONE',  ( 0.000000000000000000, 0.000000000000000000, 0.000000000000000000 ) ) ;
#4619=DIRECTION ( 'NONE',  ( 0.000000000000000000, 0.000000000000000000, 1.000000000000000000 ) ) ;
#4620=CARTESIAN_POINT ( 'NONE',  ( 0.000000000000000000, 25.00000000000000000, -7.790539539321167162 ) ) ;
#4626=CARTESIAN_POINT ( 'NONE',  ( -6.011784583892834100, -22.20189362571451142, 36.28151155367954317 ) ) ;
#4631=STYLED_ITEM('',(#6419),#365);
#4636=EDGE_CURVE ( 'NONE', #5193, #3828, #818, .T. ) ;
#4642=CARTESIAN_POINT ( 'NONE',  ( 15.22537606545850508, 19.83673216789829752, 1.447296480073241076 ) ) ;
#4658=ORIENTED_EDGE ( 'NONE', *, *, #4879, .T. ) ;
#4667=PRODUCT ( 'Part 32,2_Varsay\X2\0131\X0\lan', 'Part 32,2_Varsay\X2\0131\X0\lan', '', ( #1565 ) ) ;
#4672=CARTESIAN_POINT ( 'NONE',  ( -13.85467998626346819, 20.81921389911402542, 3.398299129130501139 ) ) ;
#4677=CARTESIAN_POINT ( 'NONE',  ( -5.648970382492173314, 24.35596037157667126, 26.81763994746973623 ) ) ;
#4678=FACE_OUTER_BOUND ( 'NONE', #4463, .T. ) ;
#4686=ORIENTED_EDGE ( 'NONE', *, *, #1996, .F. ) ;
#4687=EDGE_CURVE ( 'NONE', #2247, #1460, #3365, .T. ) ;
#4689=CARTESIAN_POINT ( 'NONE',  ( 8.997257985596670338, -21.18070524412206623, 7.578991052498396996 ) ) ;
#4692=ORIENTED_EDGE ( 'NONE', *, *, #4603, .T. ) ;
#4693=VECTOR ( 'NONE', #3164, 1000.000000000000000 ) ;
#4704=CARTESIAN_POINT ( 'NONE',  ( 7.307255365082232501, 23.90829471491150571, 30.06775954199970258 ) ) ;
#4708=CARTESIAN_POINT ( 'NONE',  ( 0.9883880857196321035, -24.98510658176930832, 24.32423833034778582 ) ) ;
#4710=VECTOR ( 'NONE', #3726, 1000.000000000000000 ) ;
#4718=FACE_BOUND ( 'NONE', #5974, .T. ) ;
#4724=AXIS2_PLACEMENT_3D ( 'NONE', #6303, #4327, #5761 ) ;
#4735=CARTESIAN_POINT ( 'NONE',  ( -7.401918722292613495, -23.87915698552384569, 33.00856600121881712 ) ) ;
#4739=CARTESIAN_POINT ( 'NONE',  ( 5.952041157299182039, 24.28165242506072374, 36.34480154750762182 ) ) ;
#4744=CARTESIAN_POINT ( 'NONE',  ( 7.451526880251365448, -23.86388513668106270, 30.79056676978083829 ) ) ;
#4747=CARTESIAN_POINT ( 'NONE',  ( -5.640759563529088361, 24.35584729907772683, 36.72391480687586807 ) ) ;
#4749=LINE ( 'NONE', #2396, #5953 ) ;
#4754=VERTEX_POINT ( 'NONE', #2414 ) ;
#4763=CARTESIAN_POINT ( 'NONE',  ( 0.000000000000000000, 0.000000000000000000, 44.00000000000000711 ) ) ;
#4764=ORIENTED_EDGE ( 'NONE', *, *, #5167, .F. ) ;
#4771=ORIENTED_EDGE ( 'NONE', *, *, #6189, .F. ) ;
#4772=CARTESIAN_POINT ( 'NONE',  ( -2.012341796004660122, 19.89850447888114005, 39.00000000000001421 ) ) ;
#4775=CARTESIAN_POINT ( 'NONE',  ( 6.737430854173819483, -24.07581932788624357, 28.44406090190429737 ) ) ;
#4777=ORIENTED_EDGE ( 'NONE', *, *, #5270, .F. ) ;
#4778=CARTESIAN_POINT ( 'NONE',  ( -7.245258220727285980, 23.92722011157075812, 29.82133114287520925 ) ) ;
#4789=ADVANCED_FACE ( 'NONE', ( #583, #3895 ), #5875, .T. ) ;
#4801=CARTESIAN_POINT ( 'NONE',  ( 7.257437786822880099, 23.92362332953075565, 33.72945147699581980 ) ) ;
#4803=DIRECTION ( 'NONE',  ( 1.000000000000000000, 0.000000000000000000, 0.000000000000000000 ) ) ;
#4805=CARTESIAN_POINT ( 'NONE',  ( 7.500225230914490560, -23.84840920358612948, 32.26396939133217501 ) ) ;
#4806=ORIENTED_EDGE ( 'NONE', *, *, #3257, .F. ) ;
#4813=DIRECTION ( 'NONE',  ( 0.000000000000000000, 0.000000000000000000, -1.000000000000000000 ) ) ;
#4820=CARTESIAN_POINT ( 'NONE',  ( 0.4617977782627283867, -24.99947972102657801, 9.999268903951906040 ) ) ;
#4838=ADVANCED_FACE ( 'NONE', ( #4332 ), #1373, .F. ) ;
#4840=CARTESIAN_POINT ( 'NONE',  ( 0.8980764441730644254, -22.98681745009828248, 24.31513574047610504 ) ) ;
#4842=AXIS2_PLACEMENT_3D ( 'NONE', #562, #4477, #2545 ) ;
#4849=DIRECTION ( 'NONE',  ( -1.000000000000000000, 0.000000000000000000, 0.000000000000000000 ) ) ;
#4852=FACE_OUTER_BOUND ( 'NONE', #5665, .T. ) ;
#4854=AXIS2_PLACEMENT_3D ( 'NONE', #2344, #1802, #3798 ) ;
#4855=ORIENTED_EDGE ( 'NONE', *, *, #2081, .F. ) ;
#4872=VERTEX_POINT ( 'NONE', #2912 ) ;
#4873=CARTESIAN_POINT ( 'NONE',  ( -2.450350183182338881, 22.87332759541404670, 38.87800362567253387 ) ) ;
#4874=EDGE_CURVE ( 'NONE', #1470, #554, #4885, .T. ) ;
#4878=VERTEX_POINT ( 'NONE', #6213 ) ;
#4879=EDGE_CURVE ( 'NONE', #4602, #4530, #1305, .T. ) ;
#4881=VERTEX_POINT ( 'NONE', #836 ) ;
#4883=EDGE_CURVE ( 'NONE', #5038, #861, #4416, .T. ) ;
#4884=CARTESIAN_POINT ( 'NONE',  ( -22.00000000000000000, 0.000000000000000000, 47.00000000000000711 ) ) ;
#4885=LINE ( 'NONE', #478, #5452 ) ;
#4887=CARTESIAN_POINT ( 'NONE',  ( -10.97130857767021439, -22.47473234318869473, 6.237739505811241258 ) ) ;
#4890=CARTESIAN_POINT ( 'NONE',  ( -3.065100562737908430, -22.79875969907089228, 24.91526600425119042 ) ) ;
#4902=DIRECTION ( 'NONE',  ( 0.000000000000000000, 1.000000000000000000, 0.000000000000000000 ) ) ;
#4903=ORIENTED_EDGE ( 'NONE', *, *, #2870, .F. ) ;
#4904=CARTESIAN_POINT ( 'NONE',  ( 6.012884121744077603, 22.20400618356517697, 8.958536348443306707 ) ) ;
#4916=DIRECTION ( 'NONE',  ( -0.000000000000000000, -0.000000000000000000, -1.000000000000000000 ) ) ;
#4921=CIRCLE ( 'NONE', #1940, 20.00000000000000000 ) ;
#4924=CARTESIAN_POINT ( 'NONE',  ( -0.4497881292104084494, -22.99670767401471849, 24.28508774596658526 ) ) ;
#4936=VERTEX_POINT ( 'NONE', #5469 ) ;
#4939=CARTESIAN_POINT ( 'NONE',  ( -2.012341796004660122, 22.91179784512888773, 39.00000000000001421 ) ) ;
#4941=ADVANCED_BREP_SHAPE_REPRESENTATION ( '', ( #365, #6349 ), #4174 ) ;
#4944=CARTESIAN_POINT ( 'NONE',  ( 0.000000000000000000, 0.000000000000000000, 47.00000000000000711 ) ) ;
#4947=ORIENTED_EDGE ( 'NONE', *, *, #264, .T. ) ;
#4954=CARTESIAN_POINT ( 'NONE',  ( -6.685354258535096683, -24.10283321907681753, 8.717551967824457293 ) ) ;
#4958=AXIS2_PLACEMENT_3D ( 'NONE', #3296, #857, #3321 ) ;
#4959=CARTESIAN_POINT ( 'NONE',  ( -15.99408614349810698, 16.52843635781563592, 0.000000000000000000 ) ) ;
#4960=CARTESIAN_POINT ( 'NONE',  ( 0.000000000000000000, 25.00000000000000000, 31.77501000028010125 ) ) ;
#4964=CARTESIAN_POINT ( 'NONE',  ( 6.507303803555983812, 24.13991014445887373, 28.01358234833885774 ) ) ;
#4969=CARTESIAN_POINT ( 'NONE',  ( 11.95959904370095650, 19.64922365089178768, 5.386438528827848238 ) ) ;
#4971=CARTESIAN_POINT ( 'NONE',  ( 25.00000000000000000, 3.061616997868383043E-15, 47.00000000000000711 ) ) ;
#4976=VERTEX_POINT ( 'NONE', #4980 ) ;
#4980=CARTESIAN_POINT ( 'NONE',  ( 22.00000000000000000, 2.694222958124176809E-15, 47.00000000000000711 ) ) ;
#4981=CARTESIAN_POINT ( 'NONE',  ( -15.22537606545851396, -19.83673216789829397, 1.447296480073240410 ) ) ;
#4984=CARTESIAN_POINT ( 'NONE',  ( -7.182657412981705209E-17, 20.00000000000000711, 39.27501000028011902 ) ) ;
#4988=LINE ( 'NONE', #3511, #3652 ) ;
#4996=CARTESIAN_POINT ( 'NONE',  ( -7.199721615955812837, 21.84420850452976026, 33.88807004839755166 ) ) ;
#5022=ADVANCED_FACE ( 'NONE', ( #6014 ), #3529, .T. ) ;
#5029=AXIS2_PLACEMENT_3D ( 'NONE', #274, #4619, #3681 ) ;
#5030=CARTESIAN_POINT ( 'NONE',  ( 6.807437345657000094, 21.96969009462961253, 34.93075177053970748 ) ) ;
#5033=CIRCLE ( 'NONE', #2861, 20.00000000000000000 ) ;
#5034=CARTESIAN_POINT ( 'NONE',  ( 8.206466222643914676, 23.61787042823059224, 7.999630148859496970 ) ) ;
#5038=VERTEX_POINT ( 'NONE', #2047 ) ;
#5039=ORIENTED_EDGE ( 'NONE', *, *, #865, .F. ) ;
#5061=DIRECTION ( 'NONE',  ( 1.000000000000000000, 0.000000000000000000, -0.000000000000000000 ) ) ;
#5066=CARTESIAN_POINT ( 'NONE',  ( 6.497654244294650105, 22.06338186837085402, 35.52745571863555085 ) ) ;
#5067=CARTESIAN_POINT ( 'NONE',  ( 15.63352991451900920, 19.51442596162454990, 0.7402269581920428720 ) ) ;
#5068=DIRECTION ( 'NONE',  ( 0.000000000000000000, 0.000000000000000000, -1.000000000000000000 ) ) ;
#5086=CARTESIAN_POINT ( 'NONE',  ( -6.807437345657000094, -21.96969009462961253, 34.93075177053970748 ) ) ;
#5087=ORIENTED_EDGE ( 'NONE', *, *, #1996, .T. ) ;
#5093=CARTESIAN_POINT ( 'NONE',  ( 0.000000000000000000, 0.000000000000000000, 51.00000000000002842 ) ) ;
#5095=CARTESIAN_POINT ( 'NONE',  ( -20.00000000000000000, 0.000000000000000000, 39.00000000000001421 ) ) ;
#5096=ORIENTED_EDGE ( 'NONE', *, *, #1436, .T. ) ;
#5097=DIRECTION ( 'NONE',  ( -1.000000000000000000, 0.000000000000000000, 0.000000000000000000 ) ) ;
#5099=CARTESIAN_POINT ( 'NONE',  ( -6.801000575755121069, 21.97168837322005075, 28.60528907419297084 ) ) ;
#5100=CARTESIAN_POINT ( 'NONE',  ( -3.487686359055458762, 24.77054744280749077, 9.676329747922174818 ) ) ;
#5101=CARTESIAN_POINT ( 'NONE',  ( 5.576854706809766249, -22.31420130230918986, 36.79476692679597249 ) ) ;
#5122=CARTESIAN_POINT ( 'NONE',  ( -22.00000000000000000, 0.000000000000000000, 41.00000000000000000 ) ) ;
#5126=CARTESIAN_POINT ( 'NONE',  ( -6.736606839469455821, 22.00628563274161920, 8.696944893850881542 ) ) ;
#5130=CARTESIAN_POINT ( 'NONE',  ( 13.84152781008414301, 20.82799749684992108, 3.414623522204560668 ) ) ;
#5136=VECTOR ( 'NONE', #5248, 1000.000000000000000 ) ;
#5151=CARTESIAN_POINT ( 'NONE',  ( -9.051043717164153790, -21.15747665746626183, 7.546935333285830438 ) ) ;
#5153=DIRECTION ( 'NONE',  ( -1.000000000000000000, 0.000000000000000000, 0.000000000000000000 ) ) ;
#5154=CIRCLE ( 'NONE', #2471, 25.00000000000000000 ) ;
#5167=EDGE_CURVE ( 'NONE', #6000, #775, #1431, .T. ) ;
#5170=CARTESIAN_POINT ( 'NONE',  ( -22.00000000000000000, 0.000000000000000000, 50.00000000000000711 ) ) ;
#5171=CARTESIAN_POINT ( 'NONE',  ( 7.260561981364187290, -21.82400181508864634, 33.66843689838669462 ) ) ;
#5172=ORIENTED_EDGE ( 'NONE', *, *, #196, .T. ) ;
#5174=CARTESIAN_POINT ( 'NONE',  ( -7.451526880251365448, 23.86388513668106981, 30.79056676978084184 ) ) ;
#5176=DIRECTION ( 'NONE',  ( 1.000000000000000000, 0.000000000000000000, 0.000000000000000000 ) ) ;
#5177=DIRECTION ( 'NONE',  ( 0.000000000000000000, 0.000000000000000000, -1.000000000000000000 ) ) ;
#5183=CARTESIAN_POINT ( 'NONE',  ( -1.798140372219934502, -22.93384243835984648, 9.914400014297026331 ) ) ;
#5189=DIRECTION ( 'NONE',  ( -0.000000000000000000, -0.000000000000000000, -1.000000000000000000 ) ) ;
#5192=CARTESIAN_POINT ( 'NONE',  ( -13.86188709689055543, 18.36473791091104246, 3.388952392393740354 ) ) ;
#5193=VERTEX_POINT ( 'NONE', #4059 ) ;
#5194=CARTESIAN_POINT ( 'NONE',  ( 7.451677332883843263, 23.86383568307783065, 30.79254100948601547 ) ) ;
#5195=CARTESIAN_POINT ( 'NONE',  ( 3.680439676527237136, 22.70725644061459647, 38.32515107347151684 ) ) ;
#5196=DIRECTION ( 'NONE',  ( 1.000000000000000000, 0.000000000000000000, -0.000000000000000000 ) ) ;
#5201=CARTESIAN_POINT ( 'NONE',  ( -2.421623179306581441, 24.88356973210973777, 24.67241923065277831 ) ) ;
#5202=SPHERICAL_SURFACE ( 'NONE', #797, 40.00000002749906258 ) ;
#5211=CARTESIAN_POINT ( 'NONE',  ( -11.04889961723839775, -20.18459349909284839, 6.176241220338072324 ) ) ;
#5220=CARTESIAN_POINT ( 'NONE',  ( -0.9889208576060591893, -24.98510605705583387, 24.32423630022273286 ) ) ;
#5221=ORIENTED_EDGE ( 'NONE', *, *, #3024, .T. ) ;
#5224=CARTESIAN_POINT ( 'NONE',  ( 7.114947004179564161, 23.96699118800356487, 34.19833922271499915 ) ) ;
#5230=DIRECTION ( 'NONE',  ( 0.000000000000000000, 0.000000000000000000, 1.000000000000000000 ) ) ;
#5231=CARTESIAN_POINT ( 'NONE',  ( 0.4497709217647500868, -23.00000000000000355, 24.27501000028010836 ) ) ;
#5233=ORIENTED_EDGE ( 'NONE', *, *, #5982, .F. ) ;
#5235=CARTESIAN_POINT ( 'NONE',  ( -4.953009495843456733, 24.50520187577543396, 26.13782778128490136 ) ) ;
#5244=AXIS2_PLACEMENT_3D ( 'NONE', #6334, #444, #2372 ) ;
#5247=CARTESIAN_POINT ( 'NONE',  ( 1.707452990153496275, -22.95315184250077323, 9.939577019203930774 ) ) ;
#5248=DIRECTION ( 'NONE',  ( -0.000000000000000000, -0.000000000000000000, -1.000000000000000000 ) ) ;
#5257=DIRECTION ( 'NONE',  ( -1.000000000000000000, 0.000000000000000000, 0.000000000000000000 ) ) ;
#5259=CARTESIAN_POINT ( 'NONE',  ( -5.958576596270774850, -24.28117850353844176, 27.19366677815228428 ) ) ;
#5263=EDGE_CURVE ( 'NONE', #3333, #5570, #4126, .T. ) ;
#5266=DIRECTION ( 'NONE',  ( 1.000000000000000000, 0.000000000000000000, 0.000000000000000000 ) ) ;
#5269=CARTESIAN_POINT ( 'NONE',  ( 6.506525936991935488, -24.14011651440023698, 28.01231256153108973 ) ) ;
#5270=EDGE_CURVE ( 'NONE', #3869, #4602, #3903, .T. ) ;
#5274=CARTESIAN_POINT ( 'NONE',  ( -7.101515257722369689, 23.97027555112600083, 29.35032263750040116 ) ) ;
#5278=EDGE_CURVE ( 'NONE', #5632, #414, #1856, .T. ) ;
#5280=ORIENTED_EDGE ( 'NONE', *, *, #2532, .T. ) ;
#5292=CARTESIAN_POINT ( 'NONE',  ( -0.4985038669289053592, -25.00000000000000000, 24.27501000028010480 ) ) ;
#5295=CARTESIAN_POINT ( 'NONE',  ( 0.000000000000000000, 0.000000000000000000, 50.00000000000000711 ) ) ;
#5297=CARTESIAN_POINT ( 'NONE',  ( 5.951225761847369178, -24.28185285436556740, 36.34586759703543635 ) ) ;
#5300=CARTESIAN_POINT ( 'NONE',  ( -3.329879077396675324, 24.78142485916625049, 38.51307783140498486 ) ) ;
#5306=ORIENTED_EDGE ( 'NONE', *, *, #2848, .T. ) ;
#5308=DIRECTION ( 'NONE',  ( -0.000000000000000000, -0.000000000000000000, -1.000000000000000000 ) ) ;
#5318=CARTESIAN_POINT ( 'NONE',  ( -3.474965785108256267, -22.73929270720903872, 25.11363447059788712 ) ) ;
#5326=PLANE ( 'NONE',  #1936 ) ;
#5328=CARTESIAN_POINT ( 'NONE',  ( 7.269041597172756219, -21.82161019007790514, 29.87399971471650062 ) ) ;
#5334=CARTESIAN_POINT ( 'NONE',  ( 2.546401178541497462E-16, 25.00000000000000000, 24.27501000028010125 ) ) ;
#5335=DIRECTION ( 'NONE',  ( -0.000000000000000000, -0.000000000000000000, -1.000000000000000000 ) ) ;
#5345=CARTESIAN_POINT ( 'NONE',  ( -1.698285149303729868, -24.95717370495094301, 9.939986931234113143 ) ) ;
#5347=EDGE_CURVE ( 'NONE', #4878, #53, #4749, .T. ) ;
#5355=EDGE_CURVE ( 'NONE', #4976, #414, #504, .T. ) ;
#5357=VERTEX_POINT ( 'NONE', #794 ) ;
#5362=PLANE ( 'NONE',  #2781 ) ;
#5365=CARTESIAN_POINT ( 'NONE',  ( 7.245258220727284204, -23.92722011157075457, 29.82133114287520215 ) ) ;
#5372=DIRECTION ( 'NONE',  ( -1.000000000000000000, 0.000000000000000000, 0.000000000000000000 ) ) ;
#5381=CARTESIAN_POINT ( 'NONE',  ( 5.542644329336980036, -24.38138258431391847, 9.119897054702292394 ) ) ;
#5382=ORIENTED_EDGE ( 'NONE', *, *, #1801, .F. ) ;
#5385=CARTESIAN_POINT ( 'NONE',  ( -7.412736743525290883, -21.77298136741688950, 33.00284858769864371 ) ) ;
#5387=DIRECTION ( 'NONE',  ( 0.000000000000000000, 0.000000000000000000, -1.000000000000000000 ) ) ;
#5388=ORIENTED_EDGE ( 'NONE', *, *, #3991, .F. ) ;
#5391=CARTESIAN_POINT ( 'NONE',  ( -2.012341796004660122, 22.91179784512888773, 39.00000000000001421 ) ) ;
#5392=DIRECTION ( 'NONE',  ( 1.000000000000000000, 0.000000000000000000, 0.000000000000000000 ) ) ;
#5395=ORIENTED_EDGE ( 'NONE', *, *, #3024, .F. ) ;
#5399=LINE ( 'NONE', #2039, #288 ) ;
#5400=LINE ( 'NONE', #1983, #1220 ) ;
#5401=ORIENTED_EDGE ( 'NONE', *, *, #2582, .F. ) ;
#5408=ORIENTED_EDGE ( 'NONE', *, *, #1913, .F. ) ;
#5411=FACE_BOUND ( 'NONE', #498, .T. ) ;
#5421=FACE_OUTER_BOUND ( 'NONE', #2283, .T. ) ;
#5424=EDGE_LOOP ( 'NONE', ( #3136, #1408, #5408, #3687, #2441, #1239, #4420, #884, #3773 ) ) ;
#5429=CIRCLE ( 'NONE', #2124, 22.00000000000000000 ) ;
#5432=FACE_OUTER_BOUND ( 'NONE', #4381, .T. ) ;
#5433=ORIENTED_EDGE ( 'NONE', *, *, #3936, .F. ) ;
#5440=CIRCLE ( 'NONE', #2645, 25.00000000000000000 ) ;
#5441=CARTESIAN_POINT ( 'NONE',  ( 7.127827911436781072, -23.96564785266028963, 8.515057432034144114 ) ) ;
#5451=LINE ( 'NONE', #6024, #6025 ) ;
#5452=VECTOR ( 'NONE', #2433, 1000.000000000000000 ) ;
#5455=ORIENTED_EDGE ( 'NONE', *, *, #980, .F. ) ;
#5457=CARTESIAN_POINT ( 'NONE',  ( 14.35983982790937219, 17.97565917864960738, 2.741545323018244940 ) ) ;
#5459=CARTESIAN_POINT ( 'NONE',  ( -4.238929854785999041, 22.60676047400609789, 37.96628288490439473 ) ) ;
#5462=DIRECTION ( 'NONE',  ( 0.000000000000000000, -1.000000000000000000, 0.000000000000000000 ) ) ;
#5467=EDGE_CURVE ( 'NONE', #775, #6017, #5399, .T. ) ;
#5469=CARTESIAN_POINT ( 'NONE',  ( -7.443729366988918004E-21, 23.00000000000000000, 24.27501000028010125 ) ) ;
#5470=CARTESIAN_POINT ( 'NONE',  ( 1.764366888834146385, -24.94145795391612452, 9.917654830493175311 ) ) ;
#5477=ORIENTED_EDGE ( 'NONE', *, *, #5355, .T. ) ;
#5481=CARTESIAN_POINT ( 'NONE',  ( -15.99408614349810698, 25.00000000000000000, -4.336808689942017736E-15 ) ) ;
#5482=ORIENTED_EDGE ( 'NONE', *, *, #3262, .F. ) ;
#5485=CARTESIAN_POINT ( 'NONE',  ( 5.266685217916866613, 22.38944685319058436, 26.43066030061579141 ) ) ;
#5487=CARTESIAN_POINT ( 'NONE',  ( 0.000000000000000000, 0.000000000000000000, 23.77500997278103512 ) ) ;
#5496=ORIENTED_EDGE ( 'NONE', *, *, #4553, .T. ) ;
#5499=CARTESIAN_POINT ( 'NONE',  ( -2.012341796004660122, -22.91179784512888773, 39.00000000000001421 ) ) ;
#5508=SPHERICAL_SURFACE ( 'NONE', #4311, 40.00000002749906258 ) ;
#5512=CARTESIAN_POINT ( 'NONE',  ( 7.502604696612909407, 21.74191879359210944, 31.88172732429694989 ) ) ;
#5513=DIRECTION ( 'NONE',  ( 0.000000000000000000, 0.000000000000000000, -1.000000000000000000 ) ) ;
#5515=ORIENTED_EDGE ( 'NONE', *, *, #3538, .T. ) ;
#5517=VECTOR ( 'NONE', #84, 1000.000000000000000 ) ;
#5534=ORIENTED_EDGE ( 'NONE', *, *, #4603, .F. ) ;
#5542=DIRECTION ( 'NONE',  ( 0.000000000000000000, 0.000000000000000000, 1.000000000000000000 ) ) ;
#5544=CARTESIAN_POINT ( 'NONE',  ( -15.63674378938990905, 16.87422613917172143, 0.7336288283346519279 ) ) ;
#5547=CARTESIAN_POINT ( 'NONE',  ( 4.599867106623924506, 22.53795783706889821, 25.83444357079220666 ) ) ;
#5550=CARTESIAN_POINT ( 'NONE',  ( 13.04517011400474757, 21.32889776003925064, 4.312637851115578513 ) ) ;
#5553=ORIENTED_EDGE ( 'NONE', *, *, #4275, .F. ) ;
#5558=DIRECTION ( 'NONE',  ( 0.000000000000000000, 0.000000000000000000, -1.000000000000000000 ) ) ;
#5567=LINE ( 'NONE', #1724, #3454 ) ;
#5570=VERTEX_POINT ( 'NONE', #4455 ) ;
#5579=CARTESIAN_POINT ( 'NONE',  ( -3.009099790203600300, 22.80648947684007410, 9.749155414846011780 ) ) ;
#5581=CARTESIAN_POINT ( 'NONE',  ( -7.059265739357024394, 21.89000174688035827, 29.23188816227238362 ) ) ;
#5582=CARTESIAN_POINT ( 'NONE',  ( -15.23040061807463630, 19.83277885499231630, 1.438641001509332717 ) ) ;
#5583=CARTESIAN_POINT ( 'NONE',  ( 4.238929854785999041, -22.60676047400609789, 37.96628288490439473 ) ) ;
#5589=CARTESIAN_POINT ( 'NONE',  ( 0.000000000000000000, 0.000000000000000000, 41.00000000000000000 ) ) ;
#5608=CARTESIAN_POINT ( 'NONE',  ( -4.600626795032661143, 22.53777557106161922, 25.83521031145350122 ) ) ;
#5609=CARTESIAN_POINT ( 'NONE',  ( -0.8953912278517158763, 24.98774879684974692, 9.982794782258025634 ) ) ;
#5618=EDGE_CURVE ( 'NONE', #5570, #1679, #2131, .T. ) ;
#5620=B_SPLINE_CURVE_WITH_KNOTS ( 'NONE', 3,
 ( #5662, #223, #1243, #6111, #5631, #6212, #3205, #3172, #1275, #5211, #3761, #5151, #804, #2749, #2173, #3731, #5693, #323, #5728, #2273, #5183, #1304, #3273, #4130, #5247, #352, #3236, #6181, #3654, #835, #2786, #2714, #4689, #283, #741, #2687, #2205, #2236, #4161, #1764, #6140, #3526 ),
 .UNSPECIFIED., .F., .F.,
 ( 4, 2, 2, 2, 2, 2, 2, 2, 2, 2, 2, 2, 2, 2, 2, 2, 2, 2, 2, 2, 4 ),
 ( 0.000000000000000000, 0.002617858692138167777, 0.005235717384276335554, 0.006544646730345418141, 0.007853576076414500728, 0.01047143476855266243, 0.01308929346069082240, 0.01439822280675990239, 0.01570715215282898758, 0.01832501084496714408, 0.01963394019103622407, 0.02094286953710530058, 0.02356072822924346055, 0.02486965757531254054, 0.02617858692138162399, 0.02879644561351977702, 0.03141430430565794046, 0.03403216299779609350, 0.03665002168993425347, 0.03926788038207241344, 0.04188573907421057341 ),
 .UNSPECIFIED. ) ;
#5622=DIRECTION ( 'NONE',  ( 1.000000000000000000, 0.000000000000000000, 0.000000000000000000 ) ) ;
#5629=EDGE_CURVE ( 'NONE', #4881, #3333, #2593, .T. ) ;
#5631=CARTESIAN_POINT ( 'NONE',  ( -13.87989846901268187, -18.35105360579683165, 3.366461006762181185 ) ) ;
#5632=VERTEX_POINT ( 'NONE', #5170 ) ;
#5634=ORIENTED_EDGE ( 'NONE', *, *, #5738, .T. ) ;
#5635=ADVANCED_FACE ( 'NONE', ( #6260, #6231 ), #5326, .F. ) ;
#5643=CARTESIAN_POINT ( 'NONE',  ( -4.293665609699220731, 22.59978795717626454, 9.479591363866271436 ) ) ;
#5645=DIRECTION ( 'NONE',  ( 0.000000000000000000, -1.000000000000000000, 0.000000000000000000 ) ) ;
#5647=CARTESIAN_POINT ( 'NONE',  ( 12.19460461707454968, 21.82662405552712315, 5.169298567843264358 ) ) ;
#5648=CARTESIAN_POINT ( 'NONE',  ( 6.980300741495532257, -21.91538084489497962, 34.52732716285097325 ) ) ;
#5652=CARTESIAN_POINT ( 'NONE',  ( -0.9837646592764054398, 24.98184996318331130, 39.21432222910941334 ) ) ;
#5660=CARTESIAN_POINT ( 'NONE',  ( 0.000000000000000000, 0.000000000000000000, 41.00000000000000000 ) ) ;
#5662=CARTESIAN_POINT ( 'NONE',  ( -15.99408614349810698, -16.52843635781563592, 0.000000000000000000 ) ) ;
#5663=ORIENTED_EDGE ( 'NONE', *, *, #3056, .T. ) ;
#5665=EDGE_LOOP ( 'NONE', ( #5233, #581, #2793, #6306 ) ) ;
#5669=CARTESIAN_POINT ( 'NONE',  ( 22.00000000000000000, 2.694222958124176809E-15, 41.00000000000000000 ) ) ;
#5672=CARTESIAN_POINT ( 'NONE',  ( -2.432532833620815182, -24.88553977760506797, 24.66355118963700122 ) ) ;
#5675=ORIENTED_EDGE ( 'NONE', *, *, #2081, .T. ) ;
#5676=CYLINDRICAL_SURFACE ( 'NONE', #1350, 7.500000000000000000 ) ;
#5680=CARTESIAN_POINT ( 'NONE',  ( 4.782950468712823699, -22.50022147858462418, 37.56939778472803226 ) ) ;
#5686=DIRECTION ( 'NONE',  ( -0.000000000000000000, -0.000000000000000000, -1.000000000000000000 ) ) ;
#5693=CARTESIAN_POINT ( 'NONE',  ( -5.608440128082920140, -22.30969483029271672, 9.098285821462422263 ) ) ;
#5703=CARTESIAN_POINT ( 'NONE',  ( -7.500037790182080499, -23.84846815096123507, 31.28125562555191763 ) ) ;
#5705=EDGE_CURVE ( 'NONE', #4530, #12, #5850, .T. ) ;
#5713=CARTESIAN_POINT ( 'NONE',  ( 3.063555513103408678, -22.79893987554409662, 24.91467890029023025 ) ) ;
#5718=CARTESIAN_POINT ( 'NONE',  ( -0.2456693407522352601, 24.99999999999999645, 39.27501000028010480 ) ) ;
#5723=AXIS2_PLACEMENT_3D ( 'NONE', #2132, #3555, #1098 ) ;
#5728=CARTESIAN_POINT ( 'NONE',  ( -3.536994606882255532, -22.74309932279132340, 9.666805580179055113 ) ) ;
#5729=CIRCLE ( 'NONE', #1506, 20.00000000000000000 ) ;
#5732=ADVANCED_FACE ( 'NONE', ( #3839 ), #1360, .F. ) ;
#5735=ORIENTED_EDGE ( 'NONE', *, *, #2856, .T. ) ;
#5738=EDGE_CURVE ( 'NONE', #1816, #3396, #5440, .T. ) ;
#5741=CARTESIAN_POINT ( 'NONE',  ( -3.769534566620170057, -24.71760338780762467, 38.27724873576356401 ) ) ;
#5744=CARTESIAN_POINT ( 'NONE',  ( 0.000000000000000000, 0.000000000000000000, 0.000000000000000000 ) ) ;
#5747=CARTESIAN_POINT ( 'NONE',  ( 4.781067518356564072, 22.50057576469317411, 37.57069195157705366 ) ) ;
#5752=CARTESIAN_POINT ( 'NONE',  ( 6.978968890507021960, -21.91580918028467195, 29.01915572147083822 ) ) ;
#5757=CARTESIAN_POINT ( 'NONE',  ( -6.506525936991941705, 24.14011651440024764, 28.01231256153109683 ) ) ;
#5759=CARTESIAN_POINT ( 'NONE',  ( 0.000000000000000000, 0.000000000000000000, 47.00000000000000711 ) ) ;
#5761=DIRECTION ( 'NONE',  ( 1.000000000000000000, 0.000000000000000000, 0.000000000000000000 ) ) ;
#5764=ADVANCED_FACE ( 'NONE', ( #1548 ), #2484, .F. ) ;
#5767=DIRECTION ( 'NONE',  ( 0.000000000000000000, 0.000000000000000000, -1.000000000000000000 ) ) ;
#5776=CARTESIAN_POINT ( 'NONE',  ( -25.00000000000000000, 0.000000000000000000, 47.00000000000000711 ) ) ;
#5777=AXIS2_PLACEMENT_3D ( 'NONE', #2175, #1081, #712 ) ;
#5778=CARTESIAN_POINT ( 'NONE',  ( -6.507303803555988253, -24.13991014445888439, 28.01358234833887195 ) ) ;
#5782=CARTESIAN_POINT ( 'NONE',  ( 4.956647734651109971, 24.50626513604599310, 37.42488445140202202 ) ) ;
#5785=CARTESIAN_POINT ( 'NONE',  ( 6.385057176062306716, -22.09706105569707191, 27.81520467947423114 ) ) ;
#5788=CARTESIAN_POINT ( 'NONE',  ( -5.474672603935806237, 24.39383812260184214, 36.90705202433113641 ) ) ;
#5797=CYLINDRICAL_SURFACE ( 'NONE', #638, 22.00000000000000000 ) ;
#5799=FACE_OUTER_BOUND ( 'NONE', #3394, .T. ) ;
#5805=CARTESIAN_POINT ( 'NONE',  ( -7.438449848406675891, -23.86776331625856429, 32.76532521224502403 ) ) ;
#5810=CARTESIAN_POINT ( 'NONE',  ( 3.466163672723409750, -22.74070890941651157, 25.10873389944362444 ) ) ;
#5820=ORIENTED_EDGE ( 'NONE', *, *, #4874, .T. ) ;
#5828=CARTESIAN_POINT ( 'NONE',  ( 8.266016972479206970, -23.60732501453302490, 7.985288904279077116 ) ) ;
#5830=EDGE_CURVE ( 'NONE', #12, #4530, #610, .T. ) ;
#5845=CARTESIAN_POINT ( 'NONE',  ( 7.369598735940123824, -21.78745483514939707, 30.31133554494096671 ) ) ;
#5847=LINE ( 'NONE', #1944, #3576 ) ;
#5849=CARTESIAN_POINT ( 'NONE',  ( -6.716176415091607232, 21.99834172012562661, 35.14285310556104491 ) ) ;
#5850=CIRCLE ( 'NONE', #3059, 25.00000000000000000 ) ;
#5853=CARTESIAN_POINT ( 'NONE',  ( 22.00000000000000000, 2.694222958124176809E-15, 50.00000000000000711 ) ) ;
#5857=ORIENTED_EDGE ( 'NONE', *, *, #2294, .F. ) ;
#5858=B_SPLINE_CURVE_WITH_KNOTS ( 'NONE', 3,
 ( #450, #999, #4924, #1413, #4466, #5929, #2851, #4890, #5318, #1377, #4369, #901, #2410, #424, #2376, #4440, #6339, #6316, #1963, #31, #3957, #1508, #3405, #59, #1898, #3857, #3373, #5869, #5385, #967, #1541, #5086, #1629, #578, #3507, #4626, #2055, #4038, #3982, #1080, #2086, #3625, #190, #5499 ),
 .UNSPECIFIED., .F., .F.,
 ( 4, 2, 2, 2, 2, 2, 2, 2, 2, 2, 2, 2, 2, 2, 2, 2, 2, 2, 2, 2, 2, 4 ),
 ( 0.02157941337148385624, 0.02225324431794266020, 0.02292707526440146415, 0.02427473715731907553, 0.02562239905023668690, 0.02697006094315429828, 0.02764389188961310223, 0.02831772283607190271, 0.02966538472898951062, 0.03033921567544831110, 0.03101304662190711506, 0.03236070851482472643, 0.03303453946128352692, 0.03370837040774233434, 0.03505603230065991449, 0.03640369419357750158, 0.03707752514003628125, 0.03775135608649506092, 0.03909901797941260637, 0.04044667987233015183, 0.04179434176524769728, 0.04314200365816523580 ),
 .UNSPECIFIED. ) ;
#5863=CARTESIAN_POINT ( 'NONE',  ( -7.831318214037678693, -23.74511713421663472, 8.189156644668287299 ) ) ;
#5869=CARTESIAN_POINT ( 'NONE',  ( -7.472848606399997706, -21.75217170649850118, 32.55500807037982725 ) ) ;
#5875=CYLINDRICAL_SURFACE ( 'NONE', #5244, 25.00000000000000000 ) ;
#5882=EDGE_LOOP ( 'NONE', ( #1120, #2413, #2266, #4264, #6139, #4134, #3911, #1388, #4806 ) ) ;
#5892=CYLINDRICAL_SURFACE ( 'NONE', #1135, 22.00000000000000000 ) ;
#5901=ORIENTED_EDGE ( 'NONE', *, *, #3262, .T. ) ;
#5907=CARTESIAN_POINT ( 'NONE',  ( 4.953190041214020845, 24.50516424074860922, 26.13799397941501113 ) ) ;
#5913=CARTESIAN_POINT ( 'NONE',  ( 9.051043717164153790, 21.15747665746626183, 7.546935333285830438 ) ) ;
#5926=CARTESIAN_POINT ( 'NONE',  ( 0.000000000000000000, 0.000000000000000000, 41.00000000000000000 ) ) ;
#5927=ORIENTED_EDGE ( 'NONE', *, *, #3271, .F. ) ;
#5929=CARTESIAN_POINT ( 'NONE',  ( -1.794389728719248733, -22.93422366650650090, 24.47880888172866065 ) ) ;
#5953=VECTOR ( 'NONE', #5335, 1000.000000000000000 ) ;
#5961=CARTESIAN_POINT ( 'NONE',  ( -2.012341796004660122, -19.89850447888114005, 39.00000000000001421 ) ) ;
#5966=CIRCLE ( 'NONE', #1854, 22.00000000000000000 ) ;
#5969=DIRECTION ( 'NONE',  ( 1.000000000000000000, 0.000000000000000000, 0.000000000000000000 ) ) ;
#5974=EDGE_LOOP ( 'NONE', ( #5482, #2868 ) ) ;
#5975=CARTESIAN_POINT ( 'NONE',  ( 1.794389728719248733, 22.93422366650650090, 24.47880888172866065 ) ) ;
#5979=VECTOR ( 'NONE', #3306, 1000.000000000000000 ) ;
#5981=ORIENTED_EDGE ( 'NONE', *, *, #4103, .F. ) ;
#5982=EDGE_CURVE ( 'NONE', #2926, #4976, #1668, .T. ) ;
#5984=CLOSED_SHELL ( 'NONE', ( #3823, #3720, #796, #6174, #2117, #3023, #4005, #1667, #3520, #4789, #4389, #3497, #5022, #3603, #3890, #3525, #5764, #255, #4068, #514, #5635, #1845, #466, #6299, #4563, #3342, #1116, #2730, #4838, #5732, #197 ) ) ;
#5995=CARTESIAN_POINT ( 'NONE',  ( -15.99408614349810698, -16.52843635781563592, 0.000000000000000000 ) ) ;
#6000=VERTEX_POINT ( 'NONE', #3665 ) ;
#6001=CARTESIAN_POINT ( 'NONE',  ( 12.82303992477784860, 19.09670753041942959, 4.547733370409773990 ) ) ;
#6004=CARTESIAN_POINT ( 'NONE',  ( 7.481756639719942648, 21.74910199390652465, 31.20551891105749931 ) ) ;
#6014=FACE_OUTER_BOUND ( 'NONE', #2029, .T. ) ;
#6017=VERTEX_POINT ( 'NONE', #5122 ) ;
#6020=CARTESIAN_POINT ( 'NONE',  ( 2.012341796004660122, 25.00000000000000000, 39.00000000000001421 ) ) ;
#6024=CARTESIAN_POINT ( 'NONE',  ( -2.012341796004660122, 25.00000000000000000, 39.00000000000001421 ) ) ;
#6025=VECTOR ( 'NONE', #6057, 1000.000000000000000 ) ;
#6029=CARTESIAN_POINT ( 'NONE',  ( 0.3392246580399980727, -19.99999999999999645, 39.27501000028010480 ) ) ;
#6032=CARTESIAN_POINT ( 'NONE',  ( -1.707452990153496275, 22.95315184250077323, 9.939577019203930774 ) ) ;
#6034=CARTESIAN_POINT ( 'NONE',  ( -7.443729366988918004E-21, 23.00000000000000000, 24.27501000028010125 ) ) ;
#6038=VERTEX_POINT ( 'NONE', #3833 ) ;
#6046=CARTESIAN_POINT ( 'NONE',  ( 0.000000000000000000, 0.000000000000000000, 41.00000000000000000 ) ) ;
#6050=AXIS2_PLACEMENT_3D ( 'NONE', #4608, #5513, #237 ) ;
#6054=FACE_OUTER_BOUND ( 'NONE', #2715, .T. ) ;
#6057=DIRECTION ( 'NONE',  ( 0.000000000000000000, -1.000000000000000000, 0.000000000000000000 ) ) ;
#6062=DIRECTION ( 'NONE',  ( -1.000000000000000000, 0.000000000000000000, 0.000000000000000000 ) ) ;
#6063=ORIENTED_EDGE ( 'NONE', *, *, #358, .T. ) ;
#6065=CARTESIAN_POINT ( 'NONE',  ( -0.8355139846970627282, 23.00151096327411793, 10.00195343045036189 ) ) ;
#6068=CARTESIAN_POINT ( 'NONE',  ( 6.137861079775116302, 22.16774101882030124, 27.44213700196646144 ) ) ;
#6070=CARTESIAN_POINT ( 'NONE',  ( -0.4617977782627312178, 24.99947972102657445, 9.999268903951904264 ) ) ;
#6071=CARTESIAN_POINT ( 'NONE',  ( 3.667391228670915382, -22.70656428659075843, 38.32101890234235242 ) ) ;
#6073=B_SPLINE_CURVE_WITH_KNOTS ( 'NONE', 3,
 ( #6034, #110, #2068, #4025, #2157, #5975, #2126, #594, #1577, #3518, #5547, #1554, #5485, #3638, #1091, #6068, #1067, #4082, #3033, #3155, #1610, #2546, #689, #1645, #6004, #3548, #5512, #3064, #2579, #1124, #4116, #5030, #3096, #5066, #656, #2638, #4606, #3188, #5747, #817, #5195, #4248, #3778, #3671 ),
 .UNSPECIFIED., .F., .F.,
 ( 4, 2, 2, 2, 2, 2, 2, 2, 2, 2, 2, 2, 2, 2, 2, 2, 2, 2, 2, 2, 2, 4 ),
 ( 0.02157941337148385624, 0.02225324431794266020, 0.02292707526440146415, 0.02427473715731907553, 0.02562239905023668690, 0.02697006094315429828, 0.02764389188961310223, 0.02831772283607190271, 0.02966538472898951062, 0.03033921567544831110, 0.03101304662190711506, 0.03236070851482472643, 0.03303453946128352692, 0.03370837040774233434, 0.03505603230065991449, 0.03640369419357750158, 0.03707752514003628125, 0.03775135608649506092, 0.03909901797941260637, 0.04044667987233015183, 0.04179434176524769728, 0.04314200365816523580 ),
 .UNSPECIFIED. ) ;
#6074=VERTEX_POINT ( 'NONE', #2822 ) ;
#6080=DIRECTION ( 'NONE',  ( 0.000000000000000000, 0.000000000000000000, 1.000000000000000000 ) ) ;
#6085=CARTESIAN_POINT ( 'NONE',  ( -25.00000000000000000, 0.000000000000000000, 55.00000000000000711 ) ) ;
#6086=CIRCLE ( 'NONE', #4958, 23.00000000000000000 ) ;
#6090=CARTESIAN_POINT ( 'NONE',  ( 22.00000000000000000, 2.694222958124176809E-15, 50.00000000000000711 ) ) ;
#6092=ORIENTED_EDGE ( 'NONE', *, *, #2739, .F. ) ;
#6096=CARTESIAN_POINT ( 'NONE',  ( -7.443729366988918004E-21, 23.00000000000000000, 24.27501000028010125 ) ) ;
#6097=CARTESIAN_POINT ( 'NONE',  ( -4.322439664174057228, 24.63752030717468600, 9.487820034421872606 ) ) ;
#6098=CARTESIAN_POINT ( 'NONE',  ( 5.723282545231354490, -22.27700230555918992, 36.62722877095559681 ) ) ;
#6101=ORIENTED_EDGE ( 'NONE', *, *, #3331, .T. ) ;
#6106=DIRECTION ( 'NONE',  ( 0.000000000000000000, -1.000000000000000000, 0.000000000000000000 ) ) ;
#6111=CARTESIAN_POINT ( 'NONE',  ( -14.35983982790937219, -17.97565917864960738, 2.741545323018244940 ) ) ;
#6119=DIRECTION ( 'NONE',  ( -1.000000000000000000, 0.000000000000000000, -0.000000000000000000 ) ) ;
#6123=CARTESIAN_POINT ( 'NONE',  ( 0.9177768309508191891, 22.98591141273915639, 9.981795115530772478 ) ) ;
#6126=CARTESIAN_POINT ( 'NONE',  ( -15.99408614349810698, 19.21429697996681796, -4.336808689942017736E-15 ) ) ;
#6127=CARTESIAN_POINT ( 'NONE',  ( 2.869322346082823660, -22.82391999846087316, 38.71877048136666843 ) ) ;
#6128=ORIENTED_EDGE ( 'NONE', *, *, #4546, .F. ) ;
#6133=CARTESIAN_POINT ( 'NONE',  ( 15.99408614349810698, 25.00000000000000000, 0.000000000000000000 ) ) ;
#6139=ORIENTED_EDGE ( 'NONE', *, *, #2739, .T. ) ;
#6140=CARTESIAN_POINT ( 'NONE',  ( 15.63674378938990905, -16.87422613917171432, 0.7336288283346513728 ) ) ;
#6143=EDGE_LOOP ( 'NONE', ( #3302, #4777, #3595, #4493 ) ) ;
#6153=CARTESIAN_POINT ( 'NONE',  ( -5.943311860187945328, 22.23481035324009270, 8.999810584836245297 ) ) ;
#6155=CARTESIAN_POINT ( 'NONE',  ( 6.734764818747090764, 24.07658780463484405, 35.11236497522016720 ) ) ;
#6158=CARTESIAN_POINT ( 'NONE',  ( 12.76907600075765536, 21.49559483975649243, 4.603672158788648439 ) ) ;
#6159=CARTESIAN_POINT ( 'NONE',  ( 7.512701611559312376, -21.73844013154226218, 31.66439142681324981 ) ) ;
#6163=ORIENTED_EDGE ( 'NONE', *, *, #1205, .T. ) ;
#6174=ADVANCED_FACE ( 'NONE', ( #3215 ), #3310, .T. ) ;
#6181=CARTESIAN_POINT ( 'NONE',  ( 4.293665609699220731, -22.59978795717626454, 9.479591363866271436 ) ) ;
#6183=CARTESIAN_POINT ( 'NONE',  ( 9.184850993605147944E-16, 25.00000000000000000, 39.27501000028010480 ) ) ;
#6189=EDGE_CURVE ( 'NONE', #3396, #4872, #1803, .T. ) ;
#6190=CARTESIAN_POINT ( 'NONE',  ( -6.737723522270822940, -24.07574026236370202, 28.44448745219711583 ) ) ;
#6191=ORIENTED_EDGE ( 'NONE', *, *, #791, .F. ) ;
#6192=DIRECTION ( 'NONE',  ( 1.000000000000000000, 0.000000000000000000, 0.000000000000000000 ) ) ;
#6198=CARTESIAN_POINT ( 'NONE',  ( 1.710351842506662612, -24.94259032362968398, 24.46851125284992889 ) ) ;
#6199=ORIENTED_EDGE ( 'NONE', *, *, #6309, .T. ) ;
#6206=ORIENTED_EDGE ( 'NONE', *, *, #8, .T. ) ;
#6212=CARTESIAN_POINT ( 'NONE',  ( -13.09536939405042055, -18.91069771112636744, 4.258167217702273355 ) ) ;
#6213=CARTESIAN_POINT ( 'NONE',  ( -25.00000000000000000, 0.000000000000000000, 41.00000000000000000 ) ) ;
#6214=ORIENTED_EDGE ( 'NONE', *, *, #222, .F. ) ;
#6224=CARTESIAN_POINT ( 'NONE',  ( -7.487557334333946102, -23.85240338065037236, 32.27275042597646859 ) ) ;
#6228=CARTESIAN_POINT ( 'NONE',  ( 6.737723522270820276, 24.07574026236370912, 28.44448745219711583 ) ) ;
#6231=FACE_BOUND ( 'NONE', #1063, .T. ) ;
#6232=CARTESIAN_POINT ( 'NONE',  ( 6.703346455576358665, -22.00175929117281015, 28.40382332099657958 ) ) ;
#6242=DIRECTION ( 'NONE',  ( 1.000000000000000000, 0.000000000000000000, 0.000000000000000000 ) ) ;
#6255=DIRECTION ( 'NONE',  ( 0.000000000000000000, 0.000000000000000000, -1.000000000000000000 ) ) ;
#6257=CARTESIAN_POINT ( 'NONE',  ( 4.580917930799680349, 24.58016474715297051, 37.73350732204200852 ) ) ;
#6260=FACE_OUTER_BOUND ( 'NONE', #354, .T. ) ;
#6261=CARTESIAN_POINT ( 'NONE',  ( -2.546401178541497462E-16, -25.00000000000000000, 24.27501000028010125 ) ) ;
#6265=CARTESIAN_POINT ( 'NONE',  ( -6.493108461366345452, 24.14236833790515036, 35.53659098058280108 ) ) ;
#6273=AXIS2_PLACEMENT_3D ( 'NONE', #1139, #5177, #765 ) ;
#6275=CARTESIAN_POINT ( 'NONE',  ( 25.00000000000000000, 3.061616997868383043E-15, 47.00000000000000711 ) ) ;
#6283=CARTESIAN_POINT ( 'NONE',  ( 2.449293599978538004E-15, 0.000000000000000000, 63.77501000028010480 ) ) ;
#6286=CARTESIAN_POINT ( 'NONE',  ( -0.4912064067414951829, -25.00000000000000355, 39.27501000028010480 ) ) ;
#6294=CARTESIAN_POINT ( 'NONE',  ( 5.133479616427196746, -24.46790356832290669, 26.30175839968469731 ) ) ;
#6298=DIRECTION ( 'NONE',  ( -0.000000000000000000, -0.000000000000000000, -1.000000000000000000 ) ) ;
#6299=ADVANCED_FACE ( 'NONE', ( #2, #5411 ), #2106, .F. ) ;
#6303=CARTESIAN_POINT ( 'NONE',  ( 0.000000000000000000, 0.000000000000000000, 0.000000000000000000 ) ) ;
#6305=EDGE_LOOP ( 'NONE', ( #3427, #5634 ) ) ;
#6306=ORIENTED_EDGE ( 'NONE', *, *, #3991, .T. ) ;
#6309=EDGE_CURVE ( 'NONE', #5632, #2926, #5429, .T. ) ;
#6312=FACE_BOUND ( 'NONE', #2183, .T. ) ;
#6315=( NAMED_UNIT ( * ) SI_UNIT ( $, .STERADIAN. ) SOLID_ANGLE_UNIT ( ) );
#6316=CARTESIAN_POINT ( 'NONE',  ( -6.703552034654557623, -22.00169986843530268, 28.40415011795442979 ) ) ;
#6317=DIRECTION ( 'NONE',  ( 0.000000000000000000, 0.000000000000000000, 1.000000000000000000 ) ) ;
#6323=CARTESIAN_POINT ( 'NONE',  ( 7.101515257722367025, -23.97027555112599728, 29.35032263750039760 ) ) ;
#6325=DIRECTION ( 'NONE',  ( -0.000000000000000000, -0.000000000000000000, -1.000000000000000000 ) ) ;
#6334=CARTESIAN_POINT ( 'NONE',  ( 0.000000000000000000, 0.000000000000000000, 41.00000000000000000 ) ) ;
#6336=CARTESIAN_POINT ( 'NONE',  ( -5.896395598744651245, -24.30897383879704066, 9.016004279442030978 ) ) ;
#6339=CARTESIAN_POINT ( 'NONE',  ( -6.383431969492757929, -22.09754339782970334, 27.81230622618427617 ) ) ;
#6341=DIRECTION ( 'NONE',  ( -1.000000000000000000, 0.000000000000000000, -0.000000000000000000 ) ) ;
#6343=CIRCLE ( 'NONE', #2834, 23.00000000000000000 ) ;
#6347=FACE_OUTER_BOUND ( 'NONE', #6305, .T. ) ;
#6349=AXIS2_PLACEMENT_3D ( 'NONE', #290, #2242, #4169 ) ;
#6355=B_SPLINE_CURVE_WITH_KNOTS ( 'NONE', 3,
 ( #6261, #883, #4708, #6198, #2387, #1847, #2830, #820, #1292, #3317, #4347, #1325, #6294, #3750, #4250, #5269, #4775, #1385, #6323, #5365, #304, #4744, #2357, #4805, #369, #3866, #2768, #403, #1880, #2324, #1905, #2290, #5297, #4283, #4317, #4225, #3259, #3780, #3291, #3347, #3809, #2033, #1549, #1459, #2448, #1007 ),
 .UNSPECIFIED., .F., .F.,
 ( 4, 2, 2, 2, 2, 2, 2, 2, 2, 2, 2, 2, 2, 2, 2, 2, 2, 2, 2, 2, 2, 2, 4 ),
 ( 2.472553540688041407E-19, 0.001474063385043937338, 0.002211095077565906116, 0.002948126770087874677, 0.004422190155131812232, 0.005159221847653780793, 0.005896253540175749354, 0.007370316925219684741, 0.008844380310263619260, 0.009581412002785590423, 0.01031844369530756506, 0.01179250708035150912, 0.01326657046539545318, 0.01474063385043939897, 0.01547766554296138054, 0.01621469723548336211, 0.01695172892800534195, 0.01768876062052732526, 0.01916282400557130575, 0.02063688739061528971, 0.02211095077565927366, 0.02284798246818127085, 0.02358501416070326456 ),
 .UNSPECIFIED. ) ;
#6413=COLOUR_RGB('Off White',0.89,0.88,0.83);
#6414=FILL_AREA_STYLE_COLOUR('',#6413);
#6415=FILL_AREA_STYLE('',(#6414));
#6416=SURFACE_STYLE_FILL_AREA(#6415);
#6417=SURFACE_SIDE_STYLE('',(#6416));
#6418=SURFACE_STYLE_USAGE(.BOTH.,#6417);
#6419=PRESENTATION_STYLE_ASSIGNMENT((#6418));
ENDSEC;
END-ISO-10303-21;
